ISO-10303-21;
HEADER;
/* Generated by software containing ST-Developer
 * from STEP Tools, Inc. (www.steptools.com) 
 */

FILE_DESCRIPTION(
/* description */ (''),
/* implementation_level */ '2;1');

FILE_NAME(
/* name */ 'Hex nut M4.step',
/* time_stamp */ '2026-11-15T21:02:08-08:00',
/* author */ (''),
/* organization */ (''),
/* preprocessor_version */ 'ST-DEVELOPER v20.2',
/* originating_system */ 'Autodesk Translation Framework v15.17.0.0',
/* authorisation */ '');

FILE_SCHEMA (('AUTOMOTIVE_DESIGN { 1 0 10303 214 3 1 1 }'));
ENDSEC;

DATA;
#10=MECHANICAL_DESIGN_GEOMETRIC_PRESENTATION_REPRESENTATION('',(#612),#31566);
#141=B_SPLINE_SURFACE_WITH_KNOTS('',3,3,((#30599,#30600,#30601,#30602,#30603,
#30604,#30605,#30606,#30607,#30608,#30609,#30610,#30611,#30612,#30613,#30614,
#30615,#30616,#30617,#30618,#30619,#30620,#30621,#30622,#30623,#30624,#30625,
#30626,#30627,#30628,#30629,#30630,#30631,#30632,#30633,#30634,#30635,#30636,
#30637,#30638,#30639),(#30640,#30641,#30642,#30643,#30644,#30645,#30646,
#30647,#30648,#30649,#30650,#30651,#30652,#30653,#30654,#30655,#30656,#30657,
#30658,#30659,#30660,#30661,#30662,#30663,#30664,#30665,#30666,#30667,#30668,
#30669,#30670,#30671,#30672,#30673,#30674,#30675,#30676,#30677,#30678,#30679,
#30680),(#30681,#30682,#30683,#30684,#30685,#30686,#30687,#30688,#30689,
#30690,#30691,#30692,#30693,#30694,#30695,#30696,#30697,#30698,#30699,#30700,
#30701,#30702,#30703,#30704,#30705,#30706,#30707,#30708,#30709,#30710,#30711,
#30712,#30713,#30714,#30715,#30716,#30717,#30718,#30719,#30720,#30721),
(#30722,#30723,#30724,#30725,#30726,#30727,#30728,#30729,#30730,#30731,
#30732,#30733,#30734,#30735,#30736,#30737,#30738,#30739,#30740,#30741,#30742,
#30743,#30744,#30745,#30746,#30747,#30748,#30749,#30750,#30751,#30752,#30753,
#30754,#30755,#30756,#30757,#30758,#30759,#30760,#30761,#30762)),
 .UNSPECIFIED.,.F.,.F.,.F.,(4,4),(4,1,1,1,1,1,1,1,1,1,1,1,1,1,1,1,1,1,1,
1,1,1,1,1,1,1,1,1,1,1,1,1,1,1,1,1,1,1,4),(-0.000343277739397919,0.0451836381137164),
(11.8612367265173,12.8594360281068,13.8572920519568,14.8551480758068,15.8530040996568,
16.8508601235068,17.8487161473568,18.8465721712069,19.8444281950569,20.8422842189069,
21.8401402427569,22.8379962666069,23.8358522904569,24.833708314307,25.831564338157,
26.829420362007,27.827276385857,28.825132409707,29.822988433557,30.8208444574071,
31.8187004812571,32.8165565051071,33.8144125289571,34.8122685528071,35.8101245766571,
36.8079806005072,37.8058366243572,38.8036926482072,39.8015486720572,40.7994046959072,
41.7972607197572,42.7951167436073,43.7929727674573,44.7908287913073,45.7886848151573,
46.7865408390073,47.7843968628573,48.7822528867074,49.7801089105574),
 .UNSPECIFIED.);
#142=B_SPLINE_SURFACE_WITH_KNOTS('',3,3,((#30864,#30865,#30866,#30867,#30868,
#30869,#30870,#30871,#30872,#30873,#30874,#30875,#30876,#30877,#30878,#30879,
#30880,#30881,#30882,#30883,#30884,#30885,#30886,#30887,#30888,#30889,#30890,
#30891,#30892,#30893,#30894,#30895,#30896,#30897,#30898,#30899,#30900,#30901,
#30902,#30903,#30904),(#30905,#30906,#30907,#30908,#30909,#30910,#30911,
#30912,#30913,#30914,#30915,#30916,#30917,#30918,#30919,#30920,#30921,#30922,
#30923,#30924,#30925,#30926,#30927,#30928,#30929,#30930,#30931,#30932,#30933,
#30934,#30935,#30936,#30937,#30938,#30939,#30940,#30941,#30942,#30943,#30944,
#30945),(#30946,#30947,#30948,#30949,#30950,#30951,#30952,#30953,#30954,
#30955,#30956,#30957,#30958,#30959,#30960,#30961,#30962,#30963,#30964,#30965,
#30966,#30967,#30968,#30969,#30970,#30971,#30972,#30973,#30974,#30975,#30976,
#30977,#30978,#30979,#30980,#30981,#30982,#30983,#30984,#30985,#30986),
(#30987,#30988,#30989,#30990,#30991,#30992,#30993,#30994,#30995,#30996,
#30997,#30998,#30999,#31000,#31001,#31002,#31003,#31004,#31005,#31006,#31007,
#31008,#31009,#31010,#31011,#31012,#31013,#31014,#31015,#31016,#31017,#31018,
#31019,#31020,#31021,#31022,#31023,#31024,#31025,#31026,#31027)),
 .UNSPECIFIED.,.F.,.F.,.F.,(4,4),(4,1,1,1,1,1,1,1,1,1,1,1,1,1,1,1,1,1,1,
1,1,1,1,1,1,1,1,1,1,1,1,1,1,1,1,1,1,1,4),(-0.000237777559020256,0.0452322082991495),
(14.398141012777,15.395997036627,16.393853060477,17.391709084327,18.389565108177,
19.3874211320271,20.3852771558771,21.3831331797271,22.3809892035771,23.3788452274271,
24.3767012512771,25.3745572751272,26.3724132989772,27.3702693228272,28.3681253466772,
29.3659813705272,30.3638373943772,31.3616934182273,32.3595494420773,33.3574054659273,
34.3552614897773,35.3531175136273,36.3509735374774,37.3488295613274,38.3466855851774,
39.3445416090274,40.3423976328774,41.3402536567274,42.3381096805775,43.3359657044275,
44.3338217282775,45.3316777521275,46.3295337759775,47.3273897998275,48.3252458236776,
49.3231018475276,50.3209578713776,51.3188138952276,52.3170131439472),
 .UNSPECIFIED.);
#330=B_SPLINE_CURVE_WITH_KNOTS('',3,(#28599,#28600,#28601,#28602),
 .UNSPECIFIED.,.F.,.F.,(4,4),(49.3506092576781,49.7801089105574),
 .UNSPECIFIED.);
#331=B_SPLINE_CURVE_WITH_KNOTS('',3,(#28605,#28606,#28607,#28608,#28609,
#28610,#28611,#28612,#28613,#28614,#28615,#28616,#28617,#28618,#28619,#28620,
#28621,#28622,#28623),.UNSPECIFIED.,.F.,.F.,(4,3,3,3,3,3,4),(49.3501477946335,
49.5348989026236,49.7266884378777,49.9110953116898,50.0955292586399,50.2803754004188,
50.3020570436401),.UNSPECIFIED.);
#332=B_SPLINE_CURVE_WITH_KNOTS('',3,(#28629,#28630,#28631,#28632,#28633,
#28634,#28635,#28636,#28637,#28638,#28639,#28640,#28641,#28642,#28643,#28644,
#28645,#28646,#28647,#28648,#28649,#28650,#28651,#28652,#28653,#28654,#28655,
#28656,#28657,#28658,#28659,#28660,#28661,#28662,#28663,#28664,#28665,#28666,
#28667,#28668,#28669,#28670,#28671,#28672,#28673,#28674,#28675,#28676,#28677,
#28678,#28679,#28680,#28681,#28682,#28683,#28684,#28685,#28686,#28687,#28688,
#28689,#28690,#28691,#28692,#28693,#28694,#28695,#28696,#28697,#28698,#28699,
#28700,#28701),.UNSPECIFIED.,.F.,.F.,(4,3,3,3,3,3,3,3,3,3,3,3,3,3,3,3,3,
3,3,3,3,3,3,3,4),(43.0673059246895,43.2522056112633,43.4369952653634,43.6222398069954,
43.7929727674573,43.9782156793092,44.163074354931,44.3479065500446,44.5327226681015,
44.7179657215877,44.7908287913073,44.9757569333487,45.1602993349711,45.3448177893337,
45.5293212386388,45.7142590545009,45.7886848151573,45.9742323297121,46.1593920065477,
46.3445154630064,46.5296175368451,46.715133360823,46.7865408390073,47.000219585859,
47.1238896025612),.UNSPECIFIED.);
#333=B_SPLINE_CURVE_WITH_KNOTS('',3,(#28702,#28703,#28704,#28705,#28706,
#28707),.UNSPECIFIED.,.F.,.F.,(4,1,1,4),(47.1238898038469,47.7843968628573,
48.7822528867074,49.3506092576781),.UNSPECIFIED.);
#334=B_SPLINE_CURVE_WITH_KNOTS('',3,(#28709,#28710,#28711,#28712,#28713,
#28714,#28715,#28716,#28717,#28718,#28719,#28720,#28721,#28722,#28723,#28724,
#28725,#28726,#28727,#28728,#28729,#28730,#28731,#28732,#28733,#28734,#28735,
#28736,#28737,#28738,#28739,#28740,#28741,#28742,#28743,#28744,#28745,#28746,
#28747,#28748,#28749,#28750,#28751),.UNSPECIFIED.,.F.,.F.,(4,3,3,3,3,3,
3,3,3,3,3,3,3,3,4),(47.1238898038469,47.3273897998275,47.51231737018,47.6968591993505,
47.8813770883876,48.0658799756973,48.2508172448081,48.3252458236776,48.5107935857524,
48.6959535054872,48.8810771946655,49.0661794955925,49.2516955342477,49.3231018475276,
49.3501477946335),.UNSPECIFIED.);
#335=B_SPLINE_CURVE_WITH_KNOTS('',3,(#28752,#28753,#28754,#28755,#28756,
#28757,#28758,#28759),.UNSPECIFIED.,.F.,.F.,(4,1,1,1,1,4),(43.0658538860988,
43.3359657044275,44.3338217282775,45.3316777521275,46.3295337759775,47.1238866805092),
 .UNSPECIFIED.);
#336=B_SPLINE_CURVE_WITH_KNOTS('',3,(#28765,#28766,#28767,#28768,#28769,
#28770,#28771,#28772,#28773,#28774,#28775,#28776,#28777,#28778,#28779,#28780,
#28781,#28782,#28783,#28784,#28785,#28786,#28787,#28788,#28789,#28790,#28791,
#28792,#28793,#28794,#28795,#28796,#28797,#28798,#28799,#28800,#28801,#28802,
#28803,#28804,#28805,#28806,#28807,#28808,#28809,#28810,#28811,#28812,#28813,
#28814,#28815,#28816,#28817,#28818,#28819,#28820,#28821,#28822,#28823,#28824,
#28825,#28826,#28827,#28828,#28829,#28830,#28831,#28832,#28833,#28834,#28835,
#28836,#28837,#28838,#28839,#28840,#28841,#28842,#28843),.UNSPECIFIED.,
 .F.,.F.,(4,3,3,3,3,3,3,3,3,3,3,3,3,3,3,3,3,3,3,3,3,3,3,3,3,3,4),(36.7834219822921,
36.8079806005072,36.9931719387593,37.1779780330912,37.362756993202,37.5475194411345,
37.7327091962842,37.8058366243572,37.9910292938932,38.1758367476732,38.3606170872144,
38.5453809276248,38.7305720682194,38.8036926482072,38.9888779939723,39.1736781071512,
39.3584511917718,39.5432078181554,39.72839194028,39.8015486720572,39.9867443267892,
40.1715546811428,40.356337756726,40.5411042418332,40.7262978434319,40.7994046959072,
40.8407044966673),.UNSPECIFIED.);
#337=B_SPLINE_CURVE_WITH_KNOTS('',3,(#28844,#28845,#28846,#28847,#28848,
#28849,#28850,#28851,#28852,#28853,#28854,#28855,#28856,#28857,#28858,#28859,
#28860,#28861,#28862,#28863,#28864,#28865,#28866,#28867,#28868,#28869,#28870,
#28871,#28872,#28873,#28874,#28875,#28876,#28877,#28878,#28879,#28880,#28881,
#28882,#28883,#28884,#28885,#28886),.UNSPECIFIED.,.F.,.F.,(4,3,3,3,3,3,
3,3,3,3,3,3,3,3,4),(40.8407044969516,41.0246827204584,41.2178272202831,
41.4014105178206,41.5850067089575,41.7690121301243,41.7972607197572,41.9824130884132,
42.1671801883195,42.351920700675,42.536644970248,42.7217976592989,42.7951167436073,
42.980347380645,43.0673059246895),.UNSPECIFIED.);
#338=B_SPLINE_CURVE_WITH_KNOTS('',3,(#28888,#28889,#28890,#28891,#28892,
#28893),.UNSPECIFIED.,.F.,.F.,(4,1,1,4),(40.8407044966673,41.3402536567274,
42.3381096805775,43.0658538860988),.UNSPECIFIED.);
#339=B_SPLINE_CURVE_WITH_KNOTS('',3,(#28894,#28895,#28896,#28897,#28898,
#28899,#28900,#28901),.UNSPECIFIED.,.F.,.F.,(4,1,1,1,1,4),(36.7839118243441,
37.3488295613274,38.3466855851774,39.3445416090274,40.3423976328774,40.8407044966673),
 .UNSPECIFIED.);
#340=B_SPLINE_CURVE_WITH_KNOTS('',3,(#28907,#28908,#28909,#28910,#28911,
#28912,#28913,#28914),.UNSPECIFIED.,.F.,.F.,(4,1,1,1,1,4),(30.499580403825,
30.8208444574071,31.8187004812571,32.8165565051071,33.8144125289571,34.5575191894877),
 .UNSPECIFIED.);
#341=B_SPLINE_CURVE_WITH_KNOTS('',3,(#28915,#28916,#28917,#28918,#28919,
#28920,#28921,#28922,#28923,#28924,#28925,#28926,#28927,#28928,#28929,#28930,
#28931,#28932,#28933,#28934,#28935,#28936,#28937,#28938,#28939,#28940,#28941,
#28942,#28943,#28944,#28945,#28946,#28947,#28948,#28949,#28950,#28951,#28952,
#28953,#28954,#28955,#28956,#28957),.UNSPECIFIED.,.F.,.F.,(4,3,3,3,3,3,
3,3,3,3,3,3,3,3,4),(34.5575193250544,34.7954285477193,34.8122685528071,
34.9974597158663,35.1822656476729,35.3670444658238,35.5518067834417,35.736996427808,
35.8101245766571,35.995316001551,36.1801199401346,36.3648794202756,36.5496215205385,
36.7347510048651,36.7834219822921),.UNSPECIFIED.);
#342=B_SPLINE_CURVE_WITH_KNOTS('',3,(#28959,#28960,#28961,#28962,#28963,
#28964),.UNSPECIFIED.,.F.,.F.,(4,1,1,4),(34.557522089489,35.3531175136273,
36.3509735374774,36.7839118243441),.UNSPECIFIED.);
#343=B_SPLINE_CURVE_WITH_KNOTS('',3,(#28965,#28966,#28967,#28968,#28969,
#28970,#28971,#28972,#28973,#28974,#28975,#28976,#28977,#28978,#28979,#28980,
#28981,#28982,#28983,#28984,#28985,#28986,#28987,#28988,#28989,#28990,#28991,
#28992,#28993,#28994,#28995,#28996,#28997,#28998,#28999,#29000,#29001,#29002,
#29003,#29004,#29005,#29006,#29007,#29008,#29009,#29010,#29011,#29012,#29013,
#29014,#29015,#29016,#29017,#29018,#29019,#29020,#29021,#29022,#29023,#29024,
#29025,#29026,#29027,#29028,#29029,#29030,#29031,#29032,#29033,#29034,#29035,
#29036,#29037),.UNSPECIFIED.,.F.,.F.,(4,3,3,3,3,3,3,3,3,3,3,3,3,3,3,3,3,
3,3,3,3,3,3,3,4),(30.5009095955721,30.6857963547127,30.8706077913032,31.0553571065148,
31.2405467884087,31.3616934182273,31.5468843306913,31.7316900105254,31.9164685785166,
32.1012306467307,32.2864200475027,32.3595494420773,32.5447402838676,32.7295458923946,
32.9143243892346,33.0990863863056,33.2842757172801,33.3574054659273,33.5425963097738,
33.7274019194642,33.9121804161483,34.0969424123043,34.2821317412473,34.3552614897773,
34.5575191894877),.UNSPECIFIED.);
#344=B_SPLINE_CURVE_WITH_KNOTS('',3,(#29043,#29044,#29045,#29046,#29047,
#29048,#29049,#29050),.UNSPECIFIED.,.F.,.F.,(4,1,1,1,1,4),(24.2177779943852,
24.833708314307,25.831564338157,26.829420362007,27.827276385857,28.2743338823081),
 .UNSPECIFIED.);
#345=B_SPLINE_CURVE_WITH_KNOTS('',3,(#29051,#29052,#29053,#29054,#29055,
#29056),.UNSPECIFIED.,.F.,.F.,(4,1,1,4),(28.2743338823081,28.825132409707,
29.822988433557,30.499580403825),.UNSPECIFIED.);
#346=B_SPLINE_CURVE_WITH_KNOTS('',3,(#29058,#29059,#29060,#29061,#29062,
#29063,#29064,#29065,#29066,#29067,#29068,#29069,#29070,#29071,#29072,#29073,
#29074,#29075,#29076,#29077,#29078,#29079,#29080,#29081,#29082,#29083,#29084,
#29085,#29086,#29087,#29088,#29089,#29090,#29091,#29092,#29093,#29094,#29095,
#29096,#29097,#29098,#29099,#29100),.UNSPECIFIED.,.F.,.F.,(4,3,3,3,3,3,
3,3,3,3,3,3,3,3,4),(28.2743338823081,28.3681253466772,28.5533165056894,
28.7381224361274,28.9229012568358,29.1076635792727,29.292853231745,29.3659813705272,
29.5511722540038,29.7359779062434,29.9207564491344,30.105518493657,30.2907078733232,
30.3638373943772,30.5009095955721),.UNSPECIFIED.);
#347=B_SPLINE_CURVE_WITH_KNOTS('',3,(#29101,#29102,#29103,#29104,#29105,
#29106,#29107,#29108),.UNSPECIFIED.,.F.,.F.,(4,1,1,1,1,4),(24.2163877000371,
24.3767012512771,25.3745572751272,26.3724132989772,27.3702693228272,28.2743251167369),
 .UNSPECIFIED.);
#348=B_SPLINE_CURVE_WITH_KNOTS('',3,(#29114,#29115,#29116,#29117,#29118,
#29119),.UNSPECIFIED.,.F.,.F.,(4,1,1,4),(15.7079632679489,16.393853060477,
17.391709084327,17.9337114285602),.UNSPECIFIED.);
#349=B_SPLINE_CURVE_WITH_KNOTS('',3,(#29121,#29122,#29123,#29124,#29125),
 .UNSPECIFIED.,.F.,.F.,(4,1,4),(14.398141012777,15.395997036627,15.7079632679489),
 .UNSPECIFIED.);
#350=B_SPLINE_CURVE_WITH_KNOTS('',3,(#29129,#29130,#29131,#29132,#29133,
#29134,#29135,#29136,#29137,#29138,#29139,#29140,#29141,#29142,#29143,#29144,
#29145,#29146,#29147,#29148,#29149,#29150,#29151,#29152,#29153,#29154,#29155,
#29156,#29157,#29158,#29159,#29160,#29161,#29162),.UNSPECIFIED.,.F.,.F.,
(4,3,3,3,3,3,3,3,3,3,3,4),(13.8761928799105,14.0610251969122,14.2454741135462,
14.4298929930741,14.614300434641,14.7991186579602,14.8551480758068,15.0378750128527,
15.22034104049,15.4026395868345,15.5852458051357,15.7079632679489),
 .UNSPECIFIED.);
#351=B_SPLINE_CURVE_WITH_KNOTS('',3,(#29163,#29164,#29165,#29166,#29167,
#29168,#29169),.UNSPECIFIED.,.F.,.F.,(4,1,1,1,4),(15.7079632679489,15.8530040996568,
16.8508601235068,17.8487161473568,17.9345037532639),.UNSPECIFIED.);
#352=B_SPLINE_CURVE_WITH_KNOTS('',3,(#29176,#29177,#29178,#29179,#29180,
#29181,#29182),.UNSPECIFIED.,.F.,.F.,(4,3,4),(-35.9039115982717,-35.7093251171368,
-35.6145585437837),.UNSPECIFIED.);
#353=B_SPLINE_CURVE_WITH_KNOTS('',3,(#29188,#29189,#29190,#29191,#29192,
#29193,#29194,#29195,#29196,#29197,#29198,#29199,#29200,#29201,#29202,#29203,
#29204,#29205,#29206,#29207,#29208,#29209,#29210,#29211,#29212,#29213,#29214,
#29215,#29216,#29217,#29218,#29219,#29220,#29221,#29222,#29223,#29224,#29225,
#29226,#29227,#29228,#29229,#29230,#29231,#29232,#29233,#29234,#29235,#29236,
#29237,#29238,#29239,#29240,#29241,#29242,#29243,#29244,#29245,#29246,#29247,
#29248,#29249,#29250,#29251,#29252,#29253,#29254,#29255,#29256,#29257,#29258,
#29259,#29260,#29261,#29262,#29263,#29264,#29265,#29266),.UNSPECIFIED.,
 .F.,.F.,(4,3,3,3,3,3,3,3,3,3,3,3,3,3,3,3,3,3,3,3,3,3,3,3,3,3,4),(33.0790390540969,
33.2735762055381,33.46804344454,33.6624725923823,33.8573645120063,33.9271048109006,
34.1226408072398,34.3232208141175,34.5182959535662,34.7216283941584,34.9249608347506,
35.1203950360828,35.3210004917123,35.5160009265929,35.7194088925967,35.9228168586006,
36.1158604071302,36.3170635259603,36.5096929699558,36.7023561566481,36.8955227366531,
36.9206728824506,37.1212646060516,37.3213945687078,37.521209127055,37.7211565859618,
37.9185289063006),.UNSPECIFIED.);
#354=B_SPLINE_CURVE_WITH_KNOTS('',3,(#29269,#29270,#29271,#29272,#29273,
#29274,#29275),.UNSPECIFIED.,.F.,.F.,(4,3,4),(-35.6145585437837,-35.4203717509587,
-35.2623097995902),.UNSPECIFIED.);
#355=B_SPLINE_CURVE_WITH_KNOTS('',3,(#29276,#29277,#29278,#29279,#29280,
#29281,#29282,#29283,#29284,#29285,#29286,#29287,#29288,#29289,#29290,#29291,
#29292,#29293,#29294,#29295,#29296,#29297,#29298,#29299,#29300,#29301,#29302,
#29303,#29304,#29305,#29306,#29307,#29308,#29309,#29310,#29311,#29312,#29313,
#29314,#29315,#29316,#29317,#29318,#29319,#29320,#29321,#29322,#29323,#29324,
#29325,#29326,#29327,#29328,#29329,#29330,#29331,#29332,#29333,#29334,#29335,
#29336,#29337,#29338,#29339,#29340,#29341,#29342,#29343,#29344,#29345,#29346,
#29347,#29348,#29349,#29350,#29351,#29352,#29353,#29354,#29355,#29356,#29357,
#29358,#29359,#29360,#29361,#29362,#29363,#29364,#29365,#29366,#29367,#29368,
#29369,#29370,#29371,#29372,#29373,#29374,#29375,#29376,#29377,#29378,#29379,
#29380,#29381,#29382,#29383,#29384,#29385,#29386,#29387,#29388,#29389,#29390,
#29391,#29392,#29393,#29394,#29395,#29396,#29397,#29398,#29399,#29400,#29401,
#29402,#29403,#29404,#29405,#29406,#29407,#29408,#29409,#29410,#29411,#29412,
#29413,#29414,#29415,#29416,#29417),.UNSPECIFIED.,.F.,.F.,(4,2,2,2,2,2,
2,2,2,2,2,2,2,2,2,2,2,2,2,2,2,2,2,2,2,2,2,2,2,2,2,2,2,2,2,2,2,2,2,2,2,2,
2,2,2,2,2,2,2,2,2,2,2,2,2,2,2,2,2,2,2,2,2,2,2,2,2,2,2,2,4),(-2.09956907933678,
-2.06727823295237,-2.05113928097752,-2.04526555762392,-2.04069307487311,
-2.03395102562868,-2.0049198629128,-1.97492707024399,-1.96497929591049,
-1.9571746485176,-1.94784846270027,-1.92838554133457,-1.89840120523387,
-1.88397088568164,-1.87832989099013,-1.87386120551477,-1.86834424737194,
-1.8491586326455,-1.82144758790311,-1.80429694004099,-1.79556342272441,
-1.78779550168319,-1.77722589230856,-1.74615256112504,-1.72734733537564,
-1.71922792962137,-1.71265167434785,-1.70819167444808,-1.70255259139146,
-1.68966202158187,-1.65645274471046,-1.63785863086284,-1.62888569237065,
-1.62106710750307,-1.6108374858822,-1.58812458017681,-1.56329361085236,
-1.55008067968731,-1.54457821075647,-1.54005036449493,-1.53309163082334,
-1.51022880175722,-1.48620348032539,-1.47021600955296,-1.46160199872145,
-1.45371801381501,-1.4443719545512,-1.4054864659731,-1.38487674877509,-1.37876788363224,
-1.37474939765288,-1.36899841169059,-1.35476317763241,-1.32283037891195,
-1.30454812183421,-1.29563417016638,-1.28784056555371,-1.27742929934751,
-1.25336736896966,-1.22948832239679,-1.21652206902214,-1.211065003871,-1.20654778236472,
-1.19958918674502,-1.17700413632658,-1.15277316727466,-1.13670931451525,
-1.12808396368615,-1.12020382988944,-1.11087854057808,-1.10890790056262),
 .UNSPECIFIED.);
#356=B_SPLINE_CURVE_WITH_KNOTS('',3,(#29423,#29424,#29425,#29426,#29427,
#29428,#29429,#29430,#29431,#29432,#29433,#29434,#29435,#29436,#29437,#29438,
#29439,#29440,#29441,#29442,#29443,#29444,#29445,#29446,#29447,#29448,#29449,
#29450,#29451,#29452,#29453,#29454,#29455,#29456,#29457,#29458,#29459,#29460,
#29461,#29462,#29463,#29464,#29465,#29466,#29467,#29468,#29469,#29470,#29471,
#29472,#29473,#29474,#29475,#29476,#29477,#29478,#29479,#29480,#29481,#29482,
#29483,#29484,#29485,#29486,#29487,#29488,#29489,#29490,#29491,#29492,#29493,
#29494,#29495,#29496,#29497,#29498,#29499,#29500,#29501,#29502,#29503,#29504,
#29505,#29506,#29507,#29508,#29509,#29510,#29511,#29512,#29513,#29514,#29515,
#29516,#29517,#29518,#29519,#29520,#29521,#29522,#29523,#29524,#29525,#29526,
#29527,#29528,#29529,#29530,#29531,#29532,#29533,#29534,#29535,#29536,#29537,
#29538,#29539,#29540,#29541,#29542,#29543,#29544,#29545,#29546,#29547,#29548,
#29549,#29550,#29551,#29552,#29553,#29554,#29555,#29556,#29557,#29558,#29559,
#29560),.UNSPECIFIED.,.F.,.F.,(4,2,2,2,2,2,2,2,2,2,2,2,2,2,2,2,2,2,2,2,
2,2,2,2,2,2,2,2,2,2,2,2,2,2,2,2,2,2,2,2,2,2,2,2,2,2,2,2,2,2,2,2,2,2,2,2,
2,2,2,2,2,2,2,2,2,2,2,2,4),(-0.991433053737511,-0.977337473195815,-0.970260427033518,
-0.965731400384691,-0.960340191712212,-0.947871567324226,-0.925756726093449,
-0.899550892131357,-0.889012428469617,-0.881208946363963,-0.872368111299795,
-0.854642934878591,-0.824922087795449,-0.808102337432252,-0.802259230694242,
-0.797807958152794,-0.791593169296394,-0.767930537438954,-0.731774736881957,
-0.721763989333825,-0.713991396496742,-0.704949329826644,-0.68556844250453,
-0.648247985382728,-0.63868331559613,-0.633735303879916,-0.628985330485743,
-0.620544831051483,-0.608949905838288,-0.563842929072849,-0.554177962826543,
-0.546428881125405,-0.536981897527955,-0.513266709646065,-0.478873020045048,
-0.470893579663265,-0.466225921200858,-0.461171453087757,-0.450949690624499,
-0.43534485981113,-0.397908716123077,-0.388056142299395,-0.380303253382117,
-0.371171801678835,-0.350914210840861,-0.325483444909963,-0.308043631438932,
-0.302154028897844,-0.297706968658483,-0.291555734644497,-0.269878621440673,
-0.23047302162497,-0.22075162425777,-0.213001903003153,-0.20360740505944,
-0.180558783665135,-0.154770716380689,-0.140725473519647,-0.135006970928188,
-0.13052259975358,-0.123957933809361,-0.11587583906428,-0.0972910383236796,
-0.0662746582505576,-0.055705898203988,-0.0478817462372992,-0.03901320709763,
-0.0278029871581142,-0.000514778870911421),.UNSPECIFIED.);
#357=B_SPLINE_CURVE_WITH_KNOTS('',3,(#29561,#29562,#29563,#29564,#29565,
#29566,#29567),.UNSPECIFIED.,.F.,.F.,(4,3,4),(32.7257487910699,32.9292487870506,
33.0790390540969),.UNSPECIFIED.);
#358=B_SPLINE_CURVE_WITH_KNOTS('',3,(#29568,#29569,#29570,#29571,#29572,
#29573,#29574,#29575,#29576,#29577,#29578,#29579,#29580,#29581,#29582,#29583,
#29584,#29585,#29586,#29587,#29588,#29589,#29590,#29591,#29592,#29593,#29594,
#29595,#29596,#29597,#29598,#29599,#29600,#29601,#29602,#29603,#29604,#29605,
#29606,#29607,#29608,#29609,#29610,#29611,#29612,#29613,#29614,#29615,#29616,
#29617,#29618,#29619,#29620,#29621,#29622,#29623,#29624,#29625,#29626,#29627,
#29628,#29629,#29630,#29631,#29632,#29633,#29634,#29635,#29636,#29637,#29638,
#29639,#29640,#29641,#29642,#29643,#29644,#29645,#29646,#29647,#29648,#29649,
#29650,#29651,#29652,#29653,#29654,#29655,#29656,#29657,#29658,#29659,#29660,
#29661,#29662,#29663,#29664,#29665,#29666,#29667,#29668,#29669,#29670,#29671,
#29672,#29673,#29674,#29675,#29676,#29677,#29678,#29679,#29680,#29681,#29682,
#29683,#29684,#29685,#29686,#29687,#29688,#29689,#29690,#29691,#29692,#29693,
#29694,#29695,#29696,#29697,#29698,#29699,#29700,#29701,#29702,#29703,#29704,
#29705,#29706,#29707,#29708,#29709,#29710,#29711,#29712,#29713),
 .UNSPECIFIED.,.F.,.F.,(4,2,2,2,2,2,2,2,2,2,2,2,2,2,2,2,2,2,2,2,2,2,2,2,
2,2,2,2,2,2,2,2,2,2,2,2,2,2,2,2,2,2,2,2,2,2,2,2,2,2,2,2,2,2,2,2,2,2,2,2,
2,2,2,2,2,2,2,2,2,2,2,2,4),(-1.10890790056262,-1.08811400786465,-1.06318372338053,
-1.04994021317825,-1.04444326883627,-1.03992947342965,-1.03302212634358,
-1.01224940857337,-0.973994608384534,-0.96412889609262,-0.956366366469846,
-0.947072597747512,-0.925302220732801,-0.899983273449288,-0.884706268315308,
-0.879198964123304,-0.874720431324555,-0.869038138806254,-0.854145446547423,
-0.821608263830272,-0.804072321356126,-0.795248786020499,-0.787429498191781,
-0.77681804710707,-0.754150286556068,-0.719217613508706,-0.712560368572158,
-0.70807520733043,-0.702440706573095,-0.687999386930956,-0.657824106116089,
-0.638567692320855,-0.629385465205663,-0.621615945375873,-0.611603976187643,
-0.600215820083641,-0.576544292565914,-0.553133319059069,-0.546185319417576,
-0.541668318479214,-0.536199473415859,-0.523162722974888,-0.499025961886179,
-0.475264353138502,-0.464868363473715,-0.457070286812277,-0.448133574319588,
-0.429699580583213,-0.39710237357353,-0.383466126319985,-0.37784292645349,
-0.373356313458516,-0.366681667502665,-0.358405928620901,-0.338936199038841,
-0.309142058113764,-0.298510973793431,-0.290689197980293,-0.281874329537709,
-0.264403258376847,-0.235633820083133,-0.217992758262308,-0.2124641790746,
-0.20798318456978,-0.202320139387413,-0.187609849018096,-0.156053362441548,
-0.137688722408426,-0.128760066264379,-0.120960650483311,-0.110549993486284,
-0.0847207655443684,-0.0592711779484536),.UNSPECIFIED.);
#359=B_SPLINE_CURVE_WITH_KNOTS('',3,(#29718,#29719,#29720,#29721,#29722,
#29723,#29724,#29725,#29726,#29727,#29728,#29729,#29730,#29731,#29732,#29733,
#29734,#29735,#29736,#29737,#29738,#29739,#29740,#29741,#29742,#29743,#29744,
#29745,#29746,#29747,#29748,#29749,#29750,#29751,#29752,#29753,#29754,#29755,
#29756,#29757,#29758,#29759,#29760,#29761,#29762,#29763,#29764,#29765,#29766,
#29767,#29768,#29769,#29770,#29771,#29772,#29773,#29774,#29775,#29776,#29777,
#29778,#29779,#29780,#29781,#29782,#29783,#29784,#29785,#29786,#29787,#29788,
#29789,#29790,#29791,#29792,#29793,#29794,#29795,#29796,#29797,#29798,#29799,
#29800,#29801,#29802,#29803,#29804,#29805,#29806,#29807,#29808,#29809,#29810,
#29811,#29812,#29813,#29814,#29815,#29816,#29817,#29818,#29819,#29820,#29821,
#29822,#29823,#29824,#29825,#29826,#29827,#29828,#29829,#29830,#29831,#29832,
#29833,#29834,#29835,#29836,#29837,#29838,#29839,#29840,#29841,#29842,#29843,
#29844,#29845,#29846,#29847,#29848,#29849,#29850,#29851,#29852,#29853,#29854,
#29855,#29856,#29857,#29858,#29859,#29860,#29861,#29862,#29863),
 .UNSPECIFIED.,.F.,.F.,(4,2,2,2,2,2,2,2,2,2,2,2,2,2,2,2,2,2,2,2,2,2,2,2,
2,2,2,2,2,2,2,2,2,2,2,2,2,2,2,2,2,2,2,2,2,2,2,2,2,2,2,2,2,2,2,2,2,2,2,2,
2,2,2,2,2,2,2,2,2,2,2,2,4),(-2.04121419657881,-2.03466850023715,-1.99673483105692,
-1.97563061114487,-1.96950366710435,-1.96505311876075,-1.95912893479973,
-1.94130357244149,-1.91241050598299,-1.89490467746027,-1.88609045027922,
-1.87827899848259,-1.86767963115871,-1.83709734466832,-1.81813557854545,
-1.80997305387442,-1.80336442429608,-1.79888792552053,-1.79323567347023,
-1.77942600076917,-1.74698641198956,-1.72858684331008,-1.71965963253582,
-1.71187019235517,-1.70148838986718,-1.66783377789036,-1.65055046134357,
-1.64277192072265,-1.63638781643952,-1.63192826839746,-1.62621775383506,
-1.61184066976607,-1.58005428931297,-1.56180786107244,-1.55289974187417,
-1.54510730016148,-1.53469157129649,-1.51051515512083,-1.48675015988346,
-1.47381671776211,-1.46836454848299,-1.46385123309717,-1.45689664040709,
-1.42389683982038,-1.40208634430952,-1.3904921613322,-1.38255555364844,
-1.37411856026509,-1.35926141727359,-1.32329440306762,-1.30783293564939,
-1.30209717341356,-1.29763101975112,-1.29114574596063,-1.25980509640235,
-1.23296816746598,-1.22243465905132,-1.21463047561848,-1.2057843620489,
-1.18802610289659,-1.15578223609239,-1.14094886261482,-1.1352763545984,
-1.13080233979671,-1.12422345794836,-1.08878610807526,-1.07166119841832,
-1.05853431663075,-1.05036493253978,-1.04224445103514,-1.02943037548668,
-1.01294627034538,-0.991433053737511),.UNSPECIFIED.);
#360=B_SPLINE_CURVE_WITH_KNOTS('',3,(#29865,#29866,#29867,#29868,#29869,
#29870,#29871,#29872,#29873,#29874,#29875,#29876,#29877,#29878),
 .UNSPECIFIED.,.F.,.F.,(4,2,2,2,2,2,4),(-0.0592711779484536,-0.0517373192803024,
-0.0454235810713492,-0.0409631664080061,-0.0350813863120996,-0.0277951384227308,
-0.000495761613670239),.UNSPECIFIED.);
#361=B_SPLINE_CURVE_WITH_KNOTS('',3,(#29879,#29880,#29881,#29882,#29883,
#29884,#29885,#29886,#29887,#29888,#29889,#29890,#29891,#29892,#29893,#29894,
#29895,#29896,#29897,#29898,#29899,#29900,#29901,#29902,#29903,#29904,#29905,
#29906,#29907,#29908,#29909,#29910,#29911,#29912,#29913,#29914,#29915,#29916,
#29917,#29918,#29919,#29920,#29921,#29922,#29923,#29924,#29925,#29926,#29927,
#29928,#29929,#29930,#29931,#29932,#29933,#29934,#29935,#29936,#29937,#29938,
#29939,#29940,#29941,#29942,#29943,#29944,#29945,#29946,#29947,#29948,#29949,
#29950,#29951,#29952,#29953,#29954,#29955,#29956,#29957,#29958,#29959,#29960,
#29961,#29962,#29963,#29964,#29965,#29966,#29967,#29968,#29969,#29970,#29971,
#29972,#29973,#29974,#29975,#29976,#29977,#29978,#29979,#29980,#29981,#29982,
#29983,#29984,#29985,#29986,#29987,#29988,#29989,#29990,#29991,#29992,#29993,
#29994,#29995,#29996,#29997,#29998,#29999,#30000,#30001,#30002,#30003,#30004,
#30005,#30006,#30007,#30008,#30009,#30010,#30011,#30012,#30013,#30014,#30015,
#30016),.UNSPECIFIED.,.F.,.F.,(4,2,2,2,2,2,2,2,2,2,2,2,2,2,2,2,2,2,2,2,
2,2,2,2,2,2,2,2,2,2,2,2,2,2,2,2,2,2,2,2,2,2,2,2,2,2,2,2,2,2,2,2,2,2,2,2,
2,2,2,2,2,2,2,2,2,2,2,2,4),(-2.09995567732276,-2.08136011835908,-2.07053665316555,
-2.06158601273293,-2.05378969108546,-2.04360051766163,-2.01015146619416,
-1.98437054469011,-1.97811554025164,-1.97365723714953,-1.96783013784949,
-1.9515564402826,-1.92541936142596,-1.90465052046543,-1.8954529777995,-1.88768543248497,
-1.87786519525954,-1.8401322124454,-1.81750972601926,-1.81132166147492,
-1.80686515424378,-1.80098042609273,-1.7857588514941,-1.75491562200284,
-1.73689583871495,-1.72800966091386,-1.72020199951066,-1.70971066915749,
-1.67726454538687,-1.65096600352949,-1.64470612746598,-1.64024757279835,
-1.63442429985572,-1.61939784692932,-1.58830100529951,-1.57021851111152,
-1.561324552486,-1.5535185049408,-1.54304238166541,-1.51040648934652,-1.4851281413965,
-1.47846905065918,-1.47398367726841,-1.46835032329901,-1.45528241327861,
-1.42224637658264,-1.40371019162329,-1.39476055023921,-1.38696457802254,
-1.3765914400719,-1.34280519617554,-1.32559316132554,-1.3178297338326,-1.31145328402773,
-1.3069896735068,-1.30125938958142,-1.28677121863048,-1.25510807035848,
-1.23688904940545,-1.22797860606782,-1.22017634457431,-1.20973328775075,
-1.17671553975917,-1.15112688542641,-1.14475626310066,-1.14029309509931,
-1.13455872305219,-1.12004228789955,-1.10908322593535),.UNSPECIFIED.);
#362=B_SPLINE_CURVE_WITH_KNOTS('',3,(#30022,#30023,#30024,#30025,#30026,
#30027,#30028,#30029,#30030,#30031),.UNSPECIFIED.,.F.,.F.,(4,1,1,1,1,1,
1,4),(14.2298304186001,14.9678403577503,15.9656963816003,16.9635524054503,
17.9614084293003,18.9592644531503,19.9571204770003,20.1593781767107),
 .UNSPECIFIED.);
#363=B_SPLINE_CURVE_WITH_KNOTS('',3,(#30032,#30033,#30034,#30035,#30036,
#30037,#30038,#30039,#30040,#30041,#30042,#30043),.UNSPECIFIED.,.F.,.F.,
(4,2,2,2,2,4),(-2.10029956731405,-2.07301378137977,-2.06183096664427,-2.05296432909478,
-2.04516370709654,-2.04121419657881),.UNSPECIFIED.);
#364=B_SPLINE_CURVE_WITH_KNOTS('',3,(#30044,#30045,#30046,#30047,#30048,
#30049,#30050,#30051,#30052,#30053,#30054,#30055,#30056,#30057,#30058,#30059,
#30060,#30061,#30062,#30063,#30064,#30065,#30066,#30067,#30068,#30069,#30070,
#30071,#30072,#30073,#30074,#30075,#30076,#30077,#30078,#30079,#30080,#30081,
#30082,#30083,#30084,#30085,#30086,#30087,#30088,#30089,#30090,#30091,#30092,
#30093,#30094,#30095,#30096,#30097,#30098,#30099,#30100,#30101,#30102,#30103,
#30104,#30105,#30106,#30107,#30108,#30109,#30110,#30111,#30112,#30113,#30114,
#30115,#30116,#30117,#30118,#30119,#30120,#30121,#30122,#30123,#30124,#30125,
#30126,#30127,#30128,#30129,#30130,#30131,#30132,#30133,#30134,#30135,#30136,
#30137,#30138,#30139,#30140,#30141,#30142,#30143,#30144,#30145,#30146,#30147,
#30148,#30149,#30150,#30151,#30152,#30153,#30154,#30155,#30156,#30157,#30158,
#30159,#30160,#30161,#30162,#30163,#30164,#30165,#30166,#30167,#30168,#30169,
#30170,#30171,#30172,#30173,#30174,#30175,#30176,#30177,#30178,#30179,#30180,
#30181,#30182,#30183,#30184,#30185,#30186,#30187,#30188,#30189),
 .UNSPECIFIED.,.F.,.F.,(4,2,2,2,2,2,2,2,2,2,2,2,2,2,2,2,2,2,2,2,2,2,2,2,
2,2,2,2,2,2,2,2,2,2,2,2,2,2,2,2,2,2,2,2,2,2,2,2,2,2,2,2,2,2,2,2,2,2,2,2,
2,2,2,2,2,2,2,2,2,2,2,2,4),(-1.10908322593535,-1.09452357101242,-1.07885078350604,
-1.0664449458177,-1.05838175086237,-1.05012684182069,-1.03648745952744,
-1.01828085964119,-0.98400040133331,-0.977832177048194,-0.973376623572291,
-0.967367964568854,-0.948537902901784,-0.905845993639871,-0.896180508699763,
-0.888426608656805,-0.878967513193345,-0.855124832993121,-0.820323487666477,
-0.812662804933415,-0.808497166747434,-0.803534746221879,-0.793899404845258,
-0.779708753006532,-0.741056059669688,-0.730667222588459,-0.722870919731796,
-0.713932583421837,-0.695476049326578,-0.662770132945483,-0.649248091834972,
-0.643641549608126,-0.639153170494086,-0.632453988480397,-0.608955843683073,
-0.574070435251138,-0.563916717951346,-0.556125229568534,-0.547156900805119,
-0.528452158744065,-0.494616651173478,-0.482463992718098,-0.476898237890252,
-0.47244553617305,-0.46571806331023,-0.440737361566452,-0.407878836719139,
-0.397418838370953,-0.389615546980399,-0.380715651187146,-0.362572536864072,
-0.331206215588982,-0.316462204577392,-0.310692519780951,-0.306231790098015,
-0.299906908412369,-0.292229487452682,-0.275376974235804,-0.2408127995192,
-0.230624915535627,-0.222829372912667,-0.213879344633832,-0.195332863843477,
-0.162229644351655,-0.149311970874657,-0.143671854051328,-0.139188617244332,
-0.13254312814391,-0.124317324947088,-0.105076000220516,-0.074926734187765,
-0.0643064573797544,-0.059535086939838),.UNSPECIFIED.);
#365=B_SPLINE_CURVE_WITH_KNOTS('',3,(#30195,#30196,#30197,#30198,#30199,
#30200,#30201,#30202,#30203,#30204),.UNSPECIFIED.,.F.,.F.,(4,3,3,4),(-4.19978038454387,
-4.00487054183563,-3.99142409540007,-3.84638326369223),.UNSPECIFIED.);
#366=B_SPLINE_CURVE_WITH_KNOTS('',3,(#30206,#30207,#30208,#30209,#30210,
#30211,#30212,#30213,#30214,#30215,#30216,#30217,#30218,#30219,#30220,#30221,
#30222,#30223,#30224,#30225,#30226,#30227,#30228,#30229,#30230,#30231,#30232,
#30233,#30234,#30235,#30236,#30237,#30238,#30239,#30240,#30241,#30242,#30243,
#30244,#30245,#30246,#30247,#30248,#30249,#30250,#30251,#30252,#30253,#30254,
#30255,#30256,#30257,#30258,#30259,#30260,#30261,#30262,#30263,#30264,#30265,
#30266,#30267,#30268,#30269),.UNSPECIFIED.,.F.,.F.,(4,3,3,3,3,3,3,3,3,3,
3,3,3,3,3,3,3,3,3,3,3,4),(-3.84638326322867,-3.65397025968246,-3.46172848296446,
-3.26958860119382,-3.07703096775827,-2.99356807155005,-2.79813514545863,
-2.59752937101898,-2.40253021789293,-2.19912113279648,-1.99571204770004,
-1.80266597681147,-1.60146348857111,-1.40883152145279,-1.2161658177683,
-1.02299676263876,-0.99785602385002,-0.797266138461779,-0.597138004075606,
-0.397325262770041,-0.197379540394573,0.),.UNSPECIFIED.);
#367=B_SPLINE_CURVE_WITH_KNOTS('',3,(#30273,#30274,#30275,#30276,#30277,
#30278,#30279,#30280,#30281,#30282,#30283,#30284,#30285,#30286,#30287,#30288,
#30289,#30290,#30291,#30292,#30293,#30294,#30295,#30296,#30297,#30298,#30299,
#30300,#30301,#30302,#30303,#30304,#30305,#30306,#30307,#30308,#30309,#30310,
#30311,#30312,#30313,#30314,#30315,#30316,#30317,#30318,#30319,#30320,#30321,
#30322,#30323,#30324,#30325,#30326,#30327,#30328,#30329,#30330,#30331,#30332,
#30333,#30334,#30335,#30336,#30337,#30338,#30339,#30340,#30341,#30342,#30343,
#30344,#30345,#30346,#30347,#30348,#30349,#30350,#30351,#30352,#30353,#30354,
#30355,#30356,#30357),.UNSPECIFIED.,.F.,.F.,(4,3,3,3,3,3,3,3,3,3,3,3,3,
3,3,3,3,3,3,3,3,3,3,3,3,3,3,3,4),(2.01461730579157,2.20940053805023,2.40544242142519,
2.59977896966128,2.79667352060566,2.99356807155005,3.18907181874155,3.38965988790618,
3.58473914322286,3.78808161931147,3.99142409540007,4.18631859471067,4.38705897584553,
4.58149457188408,4.78538734556708,4.98928011925009,5.1844968224971,5.38515665264785,
5.57992515679133,5.78353064994571,5.9871361431001,6.18233678227411,6.38300062844312,
6.57775624002241,6.78137420348627,6.98499216695013,7.18245932510578,7.38773344372867,
7.59300756235157),.UNSPECIFIED.);
#368=B_SPLINE_CURVE_WITH_KNOTS('',3,(#30358,#30359,#30360,#30361,#30362,
#30363,#30364),.UNSPECIFIED.,.F.,.F.,(4,3,4),(7.59300756271701,7.81029936589963,
7.94551948382001),.UNSPECIFIED.);
#369=B_SPLINE_CURVE_WITH_KNOTS('',3,(#30367,#30368,#30369,#30370,#30371,
#30372,#30373,#30374,#30375,#30376,#30377,#30378,#30379,#30380,#30381,#30382,
#30383,#30384,#30385,#30386,#30387,#30388,#30389,#30390,#30391,#30392,#30393,
#30394,#30395,#30396,#30397,#30398,#30399,#30400,#30401,#30402,#30403,#30404,
#30405,#30406,#30407,#30408,#30409,#30410,#30411,#30412,#30413,#30414,#30415,
#30416,#30417,#30418,#30419,#30420,#30421,#30422,#30423,#30424,#30425,#30426,
#30427,#30428,#30429,#30430,#30431,#30432,#30433,#30434,#30435,#30436,#30437,
#30438,#30439,#30440,#30441,#30442,#30443,#30444,#30445,#30446,#30447,#30448,
#30449,#30450,#30451,#30452,#30453,#30454,#30455,#30456,#30457,#30458,#30459,
#30460),.UNSPECIFIED.,.F.,.F.,(4,3,3,3,3,3,3,3,3,3,3,3,3,3,3,3,3,3,3,3,
3,3,3,3,3,3,3,3,3,3,3,4),(7.94551948382001,7.98284819080014,8.17801888453478,
8.37869021706362,8.57341294492868,8.77705857978941,8.98070421465015,9.17586858267023,
9.37654149662772,9.57125816316011,9.77490920083014,9.97856023850017,10.1737145962393,
10.374390012767,10.569096013294,10.7727561378221,10.9764162623502,11.1715780438284,
11.3722516044214,11.5669653285368,11.7706188073685,11.9742722862002,12.169432598189,
12.3701065261543,12.5648187904311,12.7684735502406,12.9721283100502,13.1649388907362,
13.3574741832482,13.5498287982422,13.7425729885002,13.8761925898232),
 .UNSPECIFIED.);
#370=B_SPLINE_CURVE_WITH_KNOTS('',3,(#30461,#30462,#30463,#30464,#30465),
 .UNSPECIFIED.,.F.,.F.,(4,1,4),(13.8761928695312,13.9699843339002,14.2298304186001),
 .UNSPECIFIED.);
#371=B_SPLINE_CURVE_WITH_KNOTS('',3,(#30467,#30468,#30469,#30470,#30471,
#30472,#30473,#30474,#30475,#30476),.UNSPECIFIED.,.F.,.F.,(4,2,2,2,4),(-0.059535086939838,
-0.0564873878884514,-0.0476707125610788,-0.0301752185997041,-0.000496026846082839),
 .UNSPECIFIED.);
#372=B_SPLINE_CURVE_WITH_KNOTS('',3,(#30477,#30478,#30479,#30480,#30481,
#30482,#30483,#30484,#30485,#30486,#30487,#30488,#30489,#30490,#30491,#30492,
#30493,#30494,#30495,#30496,#30497,#30498,#30499,#30500,#30501,#30502,#30503,
#30504,#30505,#30506,#30507,#30508,#30509,#30510,#30511,#30512,#30513,#30514,
#30515,#30516,#30517,#30518,#30519,#30520,#30521,#30522,#30523,#30524,#30525,
#30526,#30527,#30528,#30529,#30530,#30531,#30532,#30533,#30534,#30535,#30536,
#30537,#30538,#30539,#30540,#30541,#30542,#30543,#30544,#30545,#30546,#30547,
#30548,#30549,#30550,#30551,#30552,#30553,#30554,#30555,#30556,#30557,#30558,
#30559,#30560,#30561,#30562,#30563,#30564,#30565,#30566,#30567),
 .UNSPECIFIED.,.F.,.F.,(4,3,3,3,3,3,3,3,3,3,3,3,3,3,3,3,3,3,3,3,3,3,3,3,
3,3,3,3,3,3,4),(-10.1295685708718,-9.97856023850017,-9.78339530381815,-9.58272253152615,
-9.38800594878533,-9.18435508171774,-8.98070421465016,-8.78553363511177,
-8.58486227403386,-8.39013959387681,-8.18649389233848,-7.98284819080014,
-7.78772887232996,-7.587044695985,-7.39237295372156,-7.18868256033584,-6.98499216695012,
-6.78978727159251,-6.58912448946941,-6.39436949264541,-6.19075281787275,
-5.9871361431001,-5.79192140739705,-5.59126108536031,-5.39649262078602,
-5.19288637001805,-4.98928011925009,-4.79190518557354,-4.59739735246488,
-4.39858886850438,-4.19978038454387),.UNSPECIFIED.);
#373=B_SPLINE_CURVE_WITH_KNOTS('',3,(#30570,#30571,#30572,#30573,#30574,
#30575,#30576,#30577),.UNSPECIFIED.,.F.,.F.,(4,1,1,1,1,4),(17.9345037532639,
18.8465721712069,19.8444281950569,20.8422842189069,21.8401402427569,21.9911485751285),
 .UNSPECIFIED.);
#374=B_SPLINE_CURVE_WITH_KNOTS('',3,(#30578,#30579,#30580,#30581,#30582,
#30583),.UNSPECIFIED.,.F.,.F.,(4,1,1,4),(21.9911485751285,22.8379962666069,
23.8358522904569,24.2177779943852),.UNSPECIFIED.);
#375=B_SPLINE_CURVE_WITH_KNOTS('',3,(#30585,#30586,#30587,#30588,#30589,
#30590),.UNSPECIFIED.,.F.,.F.,(4,1,1,4),(21.9911485751285,22.3809892035771,
23.3788452274271,24.2163877000371),.UNSPECIFIED.);
#376=B_SPLINE_CURVE_WITH_KNOTS('',3,(#30591,#30592,#30593,#30594,#30595,
#30596,#30597,#30598),.UNSPECIFIED.,.F.,.F.,(4,1,1,1,1,4),(17.9337114285602,
18.389565108177,19.3874211320271,20.3852771558771,21.3831331797271,21.9911485751285),
 .UNSPECIFIED.);
#377=B_SPLINE_CURVE_WITH_KNOTS('',3,(#30763,#30764,#30765,#30766,#30767,
#30768,#30769,#30770,#30771,#30772,#30773,#30774,#30775,#30776,#30777,#30778,
#30779,#30780,#30781,#30782,#30783,#30784,#30785,#30786,#30787,#30788,#30789,
#30790,#30791,#30792,#30793,#30794,#30795,#30796,#30797,#30798,#30799,#30800,
#30801,#30802,#30803,#30804,#30805,#30806,#30807,#30808,#30809,#30810,#30811,
#30812,#30813,#30814),.UNSPECIFIED.,.F.,.F.,(4,3,3,3,3,3,3,3,3,3,3,3,3,
3,3,3,3,4),(0.,0.0396840521457091,0.0636437457144271,0.0792335113002467,
0.0944204906890096,0.132954435400309,0.150798681725158,0.164378967463246,
0.197217246712606,0.224559338868837,0.23844204002927,0.272690357598131,
0.292926531995206,0.308438743578011,0.33189942988077,0.349623021968201,
0.375435310304714,0.378621596831395),.UNSPECIFIED.);
#378=B_SPLINE_CURVE_WITH_KNOTS('',3,(#30815,#30816,#30817,#30818,#30819,
#30820,#30821,#30822,#30823,#30824,#30825,#30826,#30827,#30828,#30829,#30830,
#30831,#30832,#30833,#30834,#30835,#30836,#30837,#30838,#30839,#30840,#30841,
#30842,#30843,#30844,#30845,#30846,#30847,#30848,#30849,#30850,#30851,#30852,
#30853,#30854,#30855,#30856,#30857,#30858,#30859,#30860,#30861,#30862,#30863),
 .UNSPECIFIED.,.F.,.F.,(4,3,3,3,3,3,3,3,3,3,3,3,3,3,3,3,4),(0.,0.0336993562020884,
0.058720674885152,0.0749541916937741,0.111295928345171,0.130052519737085,
0.144860843722413,0.177258566323581,0.196035872055023,0.216652831180755,
0.255754035742724,0.276800562011943,0.29210454494085,0.320718965530381,
0.341188801348946,0.373057649428629,0.376894338948221),.UNSPECIFIED.);
#379=B_SPLINE_CURVE_WITH_KNOTS('',3,(#31028,#31029,#31030,#31031,#31032,
#31033,#31034,#31035,#31036,#31037,#31038,#31039,#31040,#31041,#31042,#31043,
#31044,#31045,#31046,#31047,#31048,#31049,#31050,#31051,#31052,#31053,#31054,
#31055,#31056,#31057,#31058,#31059,#31060,#31061,#31062,#31063,#31064,#31065,
#31066,#31067,#31068,#31069,#31070,#31071,#31072,#31073,#31074,#31075,#31076),
 .UNSPECIFIED.,.F.,.F.,(4,3,3,3,3,3,3,3,3,3,3,3,3,3,3,3,4),(0.,0.0336994181625108,
0.0587206999399412,0.0749542011850698,0.111295952145659,0.130052464675815,
0.144860842330347,0.177258566323583,0.19603586132328,0.216652857487139,
0.255754055472513,0.276800514863678,0.292104375485169,0.32071687926599,
0.341192754041541,0.373057649428634,0.376894335898406),.UNSPECIFIED.);
#380=B_SPLINE_CURVE_WITH_KNOTS('',3,(#31077,#31078,#31079,#31080,#31081,
#31082,#31083,#31084,#31085,#31086,#31087,#31088,#31089,#31090,#31091,#31092,
#31093,#31094,#31095,#31096,#31097,#31098,#31099,#31100,#31101,#31102,#31103,
#31104,#31105,#31106,#31107,#31108,#31109,#31110,#31111,#31112,#31113,#31114,
#31115,#31116,#31117,#31118,#31119,#31120,#31121,#31122,#31123,#31124,#31125,
#31126,#31127,#31128),.UNSPECIFIED.,.F.,.F.,(4,3,3,3,3,3,3,3,3,3,3,3,3,
3,3,3,3,4),(0.,0.0396840879974647,0.0636435323828637,0.0791466588049358,
0.0941437197617132,0.13268566673474,0.150609314840976,0.164286924555333,
0.19721724671262,0.224559319465188,0.238441985208755,0.272690316482752,
0.292926560932525,0.308438754786714,0.331899421631229,0.349622992774256,
0.37543531030474,0.378621596831421),.UNSPECIFIED.);
#411=FACE_BOUND('',#1128,.T.);
#412=FACE_BOUND('',#1136,.T.);
#475=CIRCLE('',#6145,0.205475);
#476=CIRCLE('',#6151,0.205475);
#477=CIRCLE('',#6153,0.1666);
#478=CIRCLE('',#6155,0.1666);
#479=CIRCLE('',#6160,0.1666);
#553=CYLINDRICAL_SURFACE('',#6144,0.205475);
#554=CYLINDRICAL_SURFACE('',#6146,0.205475);
#555=CYLINDRICAL_SURFACE('',#6147,0.205475);
#556=CYLINDRICAL_SURFACE('',#6148,0.205475);
#557=CYLINDRICAL_SURFACE('',#6149,0.205475);
#558=CYLINDRICAL_SURFACE('',#6150,0.205475);
#559=CYLINDRICAL_SURFACE('',#6152,0.1666);
#560=CYLINDRICAL_SURFACE('',#6154,0.1666);
#561=CYLINDRICAL_SURFACE('',#6156,0.1666);
#562=CYLINDRICAL_SURFACE('',#6157,0.1666);
#563=CYLINDRICAL_SURFACE('',#6158,0.1666);
#564=CYLINDRICAL_SURFACE('',#6159,0.1666);
#565=CYLINDRICAL_SURFACE('',#6161,0.1666);
#566=CYLINDRICAL_SURFACE('',#6162,0.205475);
#582=SHAPE_REPRESENTATION_RELATIONSHIP('SRR','None',#31646,#597);
#597=ADVANCED_BREP_SHAPE_REPRESENTATION('',(#627),#31561);
#612=STYLED_ITEM('',(#31720),#627);
#627=MANIFOLD_SOLID_BREP('Body1',#5725);
#812=FACE_OUTER_BOUND('',#1111,.T.);
#813=FACE_OUTER_BOUND('',#1112,.T.);
#814=FACE_OUTER_BOUND('',#1113,.T.);
#815=FACE_OUTER_BOUND('',#1114,.T.);
#816=FACE_OUTER_BOUND('',#1115,.T.);
#817=FACE_OUTER_BOUND('',#1116,.T.);
#818=FACE_OUTER_BOUND('',#1117,.T.);
#819=FACE_OUTER_BOUND('',#1118,.T.);
#820=FACE_OUTER_BOUND('',#1119,.T.);
#821=FACE_OUTER_BOUND('',#1120,.T.);
#822=FACE_OUTER_BOUND('',#1121,.T.);
#823=FACE_OUTER_BOUND('',#1122,.T.);
#824=FACE_OUTER_BOUND('',#1123,.T.);
#825=FACE_OUTER_BOUND('',#1124,.T.);
#826=FACE_OUTER_BOUND('',#1125,.T.);
#827=FACE_OUTER_BOUND('',#1126,.T.);
#828=FACE_OUTER_BOUND('',#1127,.T.);
#829=FACE_OUTER_BOUND('',#1129,.T.);
#830=FACE_OUTER_BOUND('',#1130,.T.);
#831=FACE_OUTER_BOUND('',#1131,.T.);
#832=FACE_OUTER_BOUND('',#1132,.T.);
#833=FACE_OUTER_BOUND('',#1133,.T.);
#834=FACE_OUTER_BOUND('',#1134,.T.);
#835=FACE_OUTER_BOUND('',#1135,.T.);
#1111=EDGE_LOOP('',(#4773,#4774,#4775,#4776));
#1112=EDGE_LOOP('',(#4777,#4778,#4779,#4780,#4781,#4782));
#1113=EDGE_LOOP('',(#4783,#4784,#4785,#4786,#4787,#4788));
#1114=EDGE_LOOP('',(#4789,#4790,#4791,#4792,#4793,#4794));
#1115=EDGE_LOOP('',(#4795,#4796,#4797,#4798,#4799,#4800));
#1116=EDGE_LOOP('',(#4801,#4802,#4803,#4804,#4805,#4806));
#1117=EDGE_LOOP('',(#4807,#4808,#4809));
#1118=EDGE_LOOP('',(#4810,#4811,#4812,#4813,#4814,#4815));
#1119=EDGE_LOOP('',(#4816,#4817,#4818,#4819,#4820));
#1120=EDGE_LOOP('',(#4821,#4822,#4823,#4824,#4825));
#1121=EDGE_LOOP('',(#4826,#4827,#4828,#4829,#4830));
#1122=EDGE_LOOP('',(#4831,#4832,#4833,#4834,#4835,#4836));
#1123=EDGE_LOOP('',(#4837,#4838,#4839,#4840,#4841,#4842));
#1124=EDGE_LOOP('',(#4843,#4844,#4845,#4846,#4847,#4848));
#1125=EDGE_LOOP('',(#4849,#4850,#4851,#4852,#4853,#4854,#4855,#4856,#4857,
#4858,#4859,#4860,#4861,#4862,#4863,#4864,#4865,#4866,#4867,#4868,#4869,
#4870,#4871,#4872,#4873,#4874));
#1126=EDGE_LOOP('',(#4875,#4876,#4877,#4878,#4879,#4880,#4881,#4882,#4883,
#4884,#4885,#4886,#4887,#4888,#4889,#4890,#4891,#4892,#4893,#4894,#4895,
#4896,#4897,#4898,#4899));
#1127=EDGE_LOOP('',(#4900,#4901,#4902,#4903,#4904,#4905));
#1128=EDGE_LOOP('',(#4906,#4907,#4908,#4909));
#1129=EDGE_LOOP('',(#4910,#4911,#4912,#4913));
#1130=EDGE_LOOP('',(#4914,#4915,#4916,#4917));
#1131=EDGE_LOOP('',(#4918,#4919,#4920,#4921));
#1132=EDGE_LOOP('',(#4922,#4923,#4924,#4925));
#1133=EDGE_LOOP('',(#4926,#4927,#4928,#4929));
#1134=EDGE_LOOP('',(#4930,#4931,#4932,#4933));
#1135=EDGE_LOOP('',(#4934,#4935,#4936,#4937,#4938,#4939));
#1136=EDGE_LOOP('',(#4940,#4941,#4942,#4943,#4944));
#1534=LINE('',#28597,#2041);
#1535=LINE('',#28627,#2042);
#1536=LINE('',#28763,#2043);
#1537=LINE('',#28905,#2044);
#1538=LINE('',#29041,#2045);
#1539=LINE('',#29112,#2046);
#1540=LINE('',#29173,#2047);
#1541=LINE('',#29186,#2048);
#1542=LINE('',#29421,#2049);
#1543=LINE('',#29717,#2050);
#1544=LINE('',#30020,#2051);
#1545=LINE('',#30193,#2052);
#1546=LINE('',#31132,#2053);
#1547=LINE('',#31134,#2054);
#1548=LINE('',#31136,#2055);
#1549=LINE('',#31138,#2056);
#1550=LINE('',#31140,#2057);
#1551=LINE('',#31141,#2058);
#1552=LINE('',#31145,#2059);
#1553=LINE('',#31146,#2060);
#1554=LINE('',#31147,#2061);
#1555=LINE('',#31150,#2062);
#1556=LINE('',#31151,#2063);
#1557=LINE('',#31154,#2064);
#1558=LINE('',#31155,#2065);
#1559=LINE('',#31158,#2066);
#1560=LINE('',#31159,#2067);
#1561=LINE('',#31162,#2068);
#1562=LINE('',#31163,#2069);
#1563=LINE('',#31165,#2070);
#2041=VECTOR('',#7108,0.205475);
#2042=VECTOR('',#7113,0.205475);
#2043=VECTOR('',#7116,0.205475);
#2044=VECTOR('',#7119,0.205475);
#2045=VECTOR('',#7122,0.205475);
#2046=VECTOR('',#7125,0.205475);
#2047=VECTOR('',#7130,0.1666);
#2048=VECTOR('',#7135,0.1666);
#2049=VECTOR('',#7140,0.1666);
#2050=VECTOR('',#7143,0.1666);
#2051=VECTOR('',#7146,0.1666);
#2052=VECTOR('',#7149,0.1666);
#2053=VECTOR('',#7158,1.);
#2054=VECTOR('',#7159,1.);
#2055=VECTOR('',#7160,1.);
#2056=VECTOR('',#7161,1.);
#2057=VECTOR('',#7162,1.);
#2058=VECTOR('',#7163,1.);
#2059=VECTOR('',#7166,1.);
#2060=VECTOR('',#7167,1.);
#2061=VECTOR('',#7168,1.);
#2062=VECTOR('',#7171,1.);
#2063=VECTOR('',#7172,1.);
#2064=VECTOR('',#7175,1.);
#2065=VECTOR('',#7176,1.);
#2066=VECTOR('',#7179,1.);
#2067=VECTOR('',#7180,1.);
#2068=VECTOR('',#7183,1.);
#2069=VECTOR('',#7184,1.);
#2070=VECTOR('',#7187,1.);
#2639=VERTEX_POINT('',#28595);
#2640=VERTEX_POINT('',#28596);
#2641=VERTEX_POINT('',#28598);
#2642=VERTEX_POINT('',#28603);
#2643=VERTEX_POINT('',#28625);
#2644=VERTEX_POINT('',#28626);
#2645=VERTEX_POINT('',#28628);
#2646=VERTEX_POINT('',#28708);
#2647=VERTEX_POINT('',#28761);
#2648=VERTEX_POINT('',#28762);
#2649=VERTEX_POINT('',#28764);
#2650=VERTEX_POINT('',#28887);
#2651=VERTEX_POINT('',#28903);
#2652=VERTEX_POINT('',#28904);
#2653=VERTEX_POINT('',#28906);
#2654=VERTEX_POINT('',#28958);
#2655=VERTEX_POINT('',#29039);
#2656=VERTEX_POINT('',#29040);
#2657=VERTEX_POINT('',#29042);
#2658=VERTEX_POINT('',#29057);
#2659=VERTEX_POINT('',#29110);
#2660=VERTEX_POINT('',#29111);
#2661=VERTEX_POINT('',#29113);
#2662=VERTEX_POINT('',#29120);
#2663=VERTEX_POINT('',#29126);
#2664=VERTEX_POINT('',#29128);
#2665=VERTEX_POINT('',#29171);
#2666=VERTEX_POINT('',#29172);
#2667=VERTEX_POINT('',#29174);
#2668=VERTEX_POINT('',#29184);
#2669=VERTEX_POINT('',#29185);
#2670=VERTEX_POINT('',#29187);
#2671=VERTEX_POINT('',#29268);
#2672=VERTEX_POINT('',#29419);
#2673=VERTEX_POINT('',#29420);
#2674=VERTEX_POINT('',#29422);
#2675=VERTEX_POINT('',#29715);
#2676=VERTEX_POINT('',#29716);
#2677=VERTEX_POINT('',#29864);
#2678=VERTEX_POINT('',#30018);
#2679=VERTEX_POINT('',#30019);
#2680=VERTEX_POINT('',#30021);
#2681=VERTEX_POINT('',#30191);
#2682=VERTEX_POINT('',#30192);
#2683=VERTEX_POINT('',#30194);
#2684=VERTEX_POINT('',#30205);
#2685=VERTEX_POINT('',#30270);
#2686=VERTEX_POINT('',#30272);
#2687=VERTEX_POINT('',#30366);
#2688=VERTEX_POINT('',#30466);
#2689=VERTEX_POINT('',#30569);
#2690=VERTEX_POINT('',#30584);
#2691=VERTEX_POINT('',#31130);
#2692=VERTEX_POINT('',#31131);
#2693=VERTEX_POINT('',#31133);
#2694=VERTEX_POINT('',#31135);
#2695=VERTEX_POINT('',#31137);
#2696=VERTEX_POINT('',#31139);
#2697=VERTEX_POINT('',#31143);
#2698=VERTEX_POINT('',#31144);
#2699=VERTEX_POINT('',#31149);
#2700=VERTEX_POINT('',#31153);
#2701=VERTEX_POINT('',#31157);
#2702=VERTEX_POINT('',#31161);
#3382=EDGE_CURVE('',#2639,#2640,#1534,.T.);
#3383=EDGE_CURVE('',#2640,#2641,#330,.T.);
#3384=EDGE_CURVE('',#2642,#2641,#475,.T.);
#3385=EDGE_CURVE('',#2639,#2642,#331,.T.);
#3386=EDGE_CURVE('',#2643,#2644,#1535,.T.);
#3387=EDGE_CURVE('',#2644,#2645,#332,.T.);
#3388=EDGE_CURVE('',#2645,#2640,#333,.T.);
#3389=EDGE_CURVE('',#2646,#2639,#334,.T.);
#3390=EDGE_CURVE('',#2643,#2646,#335,.T.);
#3391=EDGE_CURVE('',#2647,#2648,#1536,.T.);
#3392=EDGE_CURVE('',#2648,#2649,#336,.T.);
#3393=EDGE_CURVE('',#2649,#2644,#337,.T.);
#3394=EDGE_CURVE('',#2650,#2643,#338,.T.);
#3395=EDGE_CURVE('',#2647,#2650,#339,.T.);
#3396=EDGE_CURVE('',#2651,#2652,#1537,.T.);
#3397=EDGE_CURVE('',#2652,#2653,#340,.T.);
#3398=EDGE_CURVE('',#2653,#2648,#341,.T.);
#3399=EDGE_CURVE('',#2654,#2647,#342,.T.);
#3400=EDGE_CURVE('',#2651,#2654,#343,.T.);
#3401=EDGE_CURVE('',#2655,#2656,#1538,.T.);
#3402=EDGE_CURVE('',#2656,#2657,#344,.T.);
#3403=EDGE_CURVE('',#2657,#2652,#345,.T.);
#3404=EDGE_CURVE('',#2658,#2651,#346,.T.);
#3405=EDGE_CURVE('',#2655,#2658,#347,.T.);
#3406=EDGE_CURVE('',#2659,#2660,#1539,.T.);
#3407=EDGE_CURVE('',#2661,#2659,#348,.T.);
#3408=EDGE_CURVE('',#2662,#2661,#349,.T.);
#3409=EDGE_CURVE('',#2663,#2662,#476,.T.);
#3410=EDGE_CURVE('',#2663,#2664,#350,.T.);
#3411=EDGE_CURVE('',#2664,#2660,#351,.T.);
#3412=EDGE_CURVE('',#2665,#2666,#1540,.T.);
#3413=EDGE_CURVE('',#2667,#2666,#477,.F.);
#3414=EDGE_CURVE('',#2667,#2665,#352,.T.);
#3415=EDGE_CURVE('',#2668,#2669,#1541,.T.);
#3416=EDGE_CURVE('',#2669,#2670,#353,.T.);
#3417=EDGE_CURVE('',#2666,#2670,#478,.F.);
#3418=EDGE_CURVE('',#2665,#2671,#354,.T.);
#3419=EDGE_CURVE('',#2671,#2668,#355,.T.);
#3420=EDGE_CURVE('',#2672,#2673,#1542,.T.);
#3421=EDGE_CURVE('',#2673,#2674,#356,.T.);
#3422=EDGE_CURVE('',#2674,#2669,#357,.T.);
#3423=EDGE_CURVE('',#2668,#2672,#358,.T.);
#3424=EDGE_CURVE('',#2675,#2676,#1543,.T.);
#3425=EDGE_CURVE('',#2676,#2673,#359,.T.);
#3426=EDGE_CURVE('',#2672,#2677,#360,.T.);
#3427=EDGE_CURVE('',#2677,#2675,#361,.T.);
#3428=EDGE_CURVE('',#2678,#2679,#1544,.T.);
#3429=EDGE_CURVE('',#2679,#2680,#362,.T.);
#3430=EDGE_CURVE('',#2680,#2676,#363,.T.);
#3431=EDGE_CURVE('',#2675,#2678,#364,.T.);
#3432=EDGE_CURVE('',#2681,#2682,#1545,.T.);
#3433=EDGE_CURVE('',#2681,#2683,#365,.T.);
#3434=EDGE_CURVE('',#2683,#2684,#366,.T.);
#3435=EDGE_CURVE('',#2685,#2684,#479,.T.);
#3436=EDGE_CURVE('',#2685,#2686,#367,.T.);
#3437=EDGE_CURVE('',#2686,#2682,#368,.T.);
#3438=EDGE_CURVE('',#2682,#2687,#369,.T.);
#3439=EDGE_CURVE('',#2687,#2679,#370,.T.);
#3440=EDGE_CURVE('',#2678,#2688,#371,.T.);
#3441=EDGE_CURVE('',#2688,#2681,#372,.T.);
#3442=EDGE_CURVE('',#2660,#2689,#373,.T.);
#3443=EDGE_CURVE('',#2689,#2656,#374,.T.);
#3444=EDGE_CURVE('',#2690,#2655,#375,.T.);
#3445=EDGE_CURVE('',#2659,#2690,#376,.T.);
#3446=EDGE_CURVE('',#2641,#2667,#377,.T.);
#3447=EDGE_CURVE('',#2684,#2663,#378,.T.);
#3448=EDGE_CURVE('',#2670,#2642,#379,.T.);
#3449=EDGE_CURVE('',#2662,#2685,#380,.T.);
#3450=EDGE_CURVE('',#2691,#2692,#1546,.T.);
#3451=EDGE_CURVE('',#2692,#2693,#1547,.T.);
#3452=EDGE_CURVE('',#2693,#2694,#1548,.T.);
#3453=EDGE_CURVE('',#2694,#2695,#1549,.T.);
#3454=EDGE_CURVE('',#2695,#2696,#1550,.T.);
#3455=EDGE_CURVE('',#2696,#2691,#1551,.T.);
#3456=EDGE_CURVE('',#2697,#2698,#1552,.T.);
#3457=EDGE_CURVE('',#2698,#2691,#1553,.T.);
#3458=EDGE_CURVE('',#2697,#2696,#1554,.T.);
#3459=EDGE_CURVE('',#2699,#2697,#1555,.T.);
#3460=EDGE_CURVE('',#2699,#2695,#1556,.T.);
#3461=EDGE_CURVE('',#2700,#2699,#1557,.T.);
#3462=EDGE_CURVE('',#2700,#2694,#1558,.T.);
#3463=EDGE_CURVE('',#2701,#2700,#1559,.T.);
#3464=EDGE_CURVE('',#2701,#2693,#1560,.T.);
#3465=EDGE_CURVE('',#2702,#2701,#1561,.T.);
#3466=EDGE_CURVE('',#2702,#2692,#1562,.T.);
#3467=EDGE_CURVE('',#2698,#2702,#1563,.T.);
#4773=ORIENTED_EDGE('',*,*,#3382,.T.);
#4774=ORIENTED_EDGE('',*,*,#3383,.T.);
#4775=ORIENTED_EDGE('',*,*,#3384,.F.);
#4776=ORIENTED_EDGE('',*,*,#3385,.F.);
#4777=ORIENTED_EDGE('',*,*,#3386,.T.);
#4778=ORIENTED_EDGE('',*,*,#3387,.T.);
#4779=ORIENTED_EDGE('',*,*,#3388,.T.);
#4780=ORIENTED_EDGE('',*,*,#3382,.F.);
#4781=ORIENTED_EDGE('',*,*,#3389,.F.);
#4782=ORIENTED_EDGE('',*,*,#3390,.F.);
#4783=ORIENTED_EDGE('',*,*,#3391,.T.);
#4784=ORIENTED_EDGE('',*,*,#3392,.T.);
#4785=ORIENTED_EDGE('',*,*,#3393,.T.);
#4786=ORIENTED_EDGE('',*,*,#3386,.F.);
#4787=ORIENTED_EDGE('',*,*,#3394,.F.);
#4788=ORIENTED_EDGE('',*,*,#3395,.F.);
#4789=ORIENTED_EDGE('',*,*,#3396,.T.);
#4790=ORIENTED_EDGE('',*,*,#3397,.T.);
#4791=ORIENTED_EDGE('',*,*,#3398,.T.);
#4792=ORIENTED_EDGE('',*,*,#3391,.F.);
#4793=ORIENTED_EDGE('',*,*,#3399,.F.);
#4794=ORIENTED_EDGE('',*,*,#3400,.F.);
#4795=ORIENTED_EDGE('',*,*,#3401,.T.);
#4796=ORIENTED_EDGE('',*,*,#3402,.T.);
#4797=ORIENTED_EDGE('',*,*,#3403,.T.);
#4798=ORIENTED_EDGE('',*,*,#3396,.F.);
#4799=ORIENTED_EDGE('',*,*,#3404,.F.);
#4800=ORIENTED_EDGE('',*,*,#3405,.F.);
#4801=ORIENTED_EDGE('',*,*,#3406,.F.);
#4802=ORIENTED_EDGE('',*,*,#3407,.F.);
#4803=ORIENTED_EDGE('',*,*,#3408,.F.);
#4804=ORIENTED_EDGE('',*,*,#3409,.F.);
#4805=ORIENTED_EDGE('',*,*,#3410,.T.);
#4806=ORIENTED_EDGE('',*,*,#3411,.T.);
#4807=ORIENTED_EDGE('',*,*,#3412,.T.);
#4808=ORIENTED_EDGE('',*,*,#3413,.F.);
#4809=ORIENTED_EDGE('',*,*,#3414,.T.);
#4810=ORIENTED_EDGE('',*,*,#3415,.T.);
#4811=ORIENTED_EDGE('',*,*,#3416,.T.);
#4812=ORIENTED_EDGE('',*,*,#3417,.F.);
#4813=ORIENTED_EDGE('',*,*,#3412,.F.);
#4814=ORIENTED_EDGE('',*,*,#3418,.T.);
#4815=ORIENTED_EDGE('',*,*,#3419,.T.);
#4816=ORIENTED_EDGE('',*,*,#3420,.T.);
#4817=ORIENTED_EDGE('',*,*,#3421,.T.);
#4818=ORIENTED_EDGE('',*,*,#3422,.T.);
#4819=ORIENTED_EDGE('',*,*,#3415,.F.);
#4820=ORIENTED_EDGE('',*,*,#3423,.T.);
#4821=ORIENTED_EDGE('',*,*,#3424,.T.);
#4822=ORIENTED_EDGE('',*,*,#3425,.T.);
#4823=ORIENTED_EDGE('',*,*,#3420,.F.);
#4824=ORIENTED_EDGE('',*,*,#3426,.T.);
#4825=ORIENTED_EDGE('',*,*,#3427,.T.);
#4826=ORIENTED_EDGE('',*,*,#3428,.T.);
#4827=ORIENTED_EDGE('',*,*,#3429,.T.);
#4828=ORIENTED_EDGE('',*,*,#3430,.T.);
#4829=ORIENTED_EDGE('',*,*,#3424,.F.);
#4830=ORIENTED_EDGE('',*,*,#3431,.T.);
#4831=ORIENTED_EDGE('',*,*,#3432,.F.);
#4832=ORIENTED_EDGE('',*,*,#3433,.T.);
#4833=ORIENTED_EDGE('',*,*,#3434,.T.);
#4834=ORIENTED_EDGE('',*,*,#3435,.F.);
#4835=ORIENTED_EDGE('',*,*,#3436,.T.);
#4836=ORIENTED_EDGE('',*,*,#3437,.T.);
#4837=ORIENTED_EDGE('',*,*,#3432,.T.);
#4838=ORIENTED_EDGE('',*,*,#3438,.T.);
#4839=ORIENTED_EDGE('',*,*,#3439,.T.);
#4840=ORIENTED_EDGE('',*,*,#3428,.F.);
#4841=ORIENTED_EDGE('',*,*,#3440,.T.);
#4842=ORIENTED_EDGE('',*,*,#3441,.T.);
#4843=ORIENTED_EDGE('',*,*,#3406,.T.);
#4844=ORIENTED_EDGE('',*,*,#3442,.T.);
#4845=ORIENTED_EDGE('',*,*,#3443,.T.);
#4846=ORIENTED_EDGE('',*,*,#3401,.F.);
#4847=ORIENTED_EDGE('',*,*,#3444,.F.);
#4848=ORIENTED_EDGE('',*,*,#3445,.F.);
#4849=ORIENTED_EDGE('',*,*,#3446,.F.);
#4850=ORIENTED_EDGE('',*,*,#3383,.F.);
#4851=ORIENTED_EDGE('',*,*,#3388,.F.);
#4852=ORIENTED_EDGE('',*,*,#3387,.F.);
#4853=ORIENTED_EDGE('',*,*,#3393,.F.);
#4854=ORIENTED_EDGE('',*,*,#3392,.F.);
#4855=ORIENTED_EDGE('',*,*,#3398,.F.);
#4856=ORIENTED_EDGE('',*,*,#3397,.F.);
#4857=ORIENTED_EDGE('',*,*,#3403,.F.);
#4858=ORIENTED_EDGE('',*,*,#3402,.F.);
#4859=ORIENTED_EDGE('',*,*,#3443,.F.);
#4860=ORIENTED_EDGE('',*,*,#3442,.F.);
#4861=ORIENTED_EDGE('',*,*,#3411,.F.);
#4862=ORIENTED_EDGE('',*,*,#3410,.F.);
#4863=ORIENTED_EDGE('',*,*,#3447,.F.);
#4864=ORIENTED_EDGE('',*,*,#3434,.F.);
#4865=ORIENTED_EDGE('',*,*,#3433,.F.);
#4866=ORIENTED_EDGE('',*,*,#3441,.F.);
#4867=ORIENTED_EDGE('',*,*,#3440,.F.);
#4868=ORIENTED_EDGE('',*,*,#3431,.F.);
#4869=ORIENTED_EDGE('',*,*,#3427,.F.);
#4870=ORIENTED_EDGE('',*,*,#3426,.F.);
#4871=ORIENTED_EDGE('',*,*,#3423,.F.);
#4872=ORIENTED_EDGE('',*,*,#3419,.F.);
#4873=ORIENTED_EDGE('',*,*,#3418,.F.);
#4874=ORIENTED_EDGE('',*,*,#3414,.F.);
#4875=ORIENTED_EDGE('',*,*,#3448,.F.);
#4876=ORIENTED_EDGE('',*,*,#3416,.F.);
#4877=ORIENTED_EDGE('',*,*,#3422,.F.);
#4878=ORIENTED_EDGE('',*,*,#3421,.F.);
#4879=ORIENTED_EDGE('',*,*,#3425,.F.);
#4880=ORIENTED_EDGE('',*,*,#3430,.F.);
#4881=ORIENTED_EDGE('',*,*,#3429,.F.);
#4882=ORIENTED_EDGE('',*,*,#3439,.F.);
#4883=ORIENTED_EDGE('',*,*,#3438,.F.);
#4884=ORIENTED_EDGE('',*,*,#3437,.F.);
#4885=ORIENTED_EDGE('',*,*,#3436,.F.);
#4886=ORIENTED_EDGE('',*,*,#3449,.F.);
#4887=ORIENTED_EDGE('',*,*,#3408,.T.);
#4888=ORIENTED_EDGE('',*,*,#3407,.T.);
#4889=ORIENTED_EDGE('',*,*,#3445,.T.);
#4890=ORIENTED_EDGE('',*,*,#3444,.T.);
#4891=ORIENTED_EDGE('',*,*,#3405,.T.);
#4892=ORIENTED_EDGE('',*,*,#3404,.T.);
#4893=ORIENTED_EDGE('',*,*,#3400,.T.);
#4894=ORIENTED_EDGE('',*,*,#3399,.T.);
#4895=ORIENTED_EDGE('',*,*,#3395,.T.);
#4896=ORIENTED_EDGE('',*,*,#3394,.T.);
#4897=ORIENTED_EDGE('',*,*,#3390,.T.);
#4898=ORIENTED_EDGE('',*,*,#3389,.T.);
#4899=ORIENTED_EDGE('',*,*,#3385,.T.);
#4900=ORIENTED_EDGE('',*,*,#3450,.T.);
#4901=ORIENTED_EDGE('',*,*,#3451,.T.);
#4902=ORIENTED_EDGE('',*,*,#3452,.T.);
#4903=ORIENTED_EDGE('',*,*,#3453,.T.);
#4904=ORIENTED_EDGE('',*,*,#3454,.T.);
#4905=ORIENTED_EDGE('',*,*,#3455,.T.);
#4906=ORIENTED_EDGE('',*,*,#3447,.T.);
#4907=ORIENTED_EDGE('',*,*,#3409,.T.);
#4908=ORIENTED_EDGE('',*,*,#3449,.T.);
#4909=ORIENTED_EDGE('',*,*,#3435,.T.);
#4910=ORIENTED_EDGE('',*,*,#3456,.T.);
#4911=ORIENTED_EDGE('',*,*,#3457,.T.);
#4912=ORIENTED_EDGE('',*,*,#3455,.F.);
#4913=ORIENTED_EDGE('',*,*,#3458,.F.);
#4914=ORIENTED_EDGE('',*,*,#3459,.T.);
#4915=ORIENTED_EDGE('',*,*,#3458,.T.);
#4916=ORIENTED_EDGE('',*,*,#3454,.F.);
#4917=ORIENTED_EDGE('',*,*,#3460,.F.);
#4918=ORIENTED_EDGE('',*,*,#3461,.T.);
#4919=ORIENTED_EDGE('',*,*,#3460,.T.);
#4920=ORIENTED_EDGE('',*,*,#3453,.F.);
#4921=ORIENTED_EDGE('',*,*,#3462,.F.);
#4922=ORIENTED_EDGE('',*,*,#3463,.T.);
#4923=ORIENTED_EDGE('',*,*,#3462,.T.);
#4924=ORIENTED_EDGE('',*,*,#3452,.F.);
#4925=ORIENTED_EDGE('',*,*,#3464,.F.);
#4926=ORIENTED_EDGE('',*,*,#3465,.T.);
#4927=ORIENTED_EDGE('',*,*,#3464,.T.);
#4928=ORIENTED_EDGE('',*,*,#3451,.F.);
#4929=ORIENTED_EDGE('',*,*,#3466,.F.);
#4930=ORIENTED_EDGE('',*,*,#3467,.T.);
#4931=ORIENTED_EDGE('',*,*,#3466,.T.);
#4932=ORIENTED_EDGE('',*,*,#3450,.F.);
#4933=ORIENTED_EDGE('',*,*,#3457,.F.);
#4934=ORIENTED_EDGE('',*,*,#3467,.F.);
#4935=ORIENTED_EDGE('',*,*,#3456,.F.);
#4936=ORIENTED_EDGE('',*,*,#3459,.F.);
#4937=ORIENTED_EDGE('',*,*,#3461,.F.);
#4938=ORIENTED_EDGE('',*,*,#3463,.F.);
#4939=ORIENTED_EDGE('',*,*,#3465,.F.);
#4940=ORIENTED_EDGE('',*,*,#3446,.T.);
#4941=ORIENTED_EDGE('',*,*,#3413,.T.);
#4942=ORIENTED_EDGE('',*,*,#3417,.T.);
#4943=ORIENTED_EDGE('',*,*,#3448,.T.);
#4944=ORIENTED_EDGE('',*,*,#3384,.T.);
#5378=PLANE('',#6163);
#5379=PLANE('',#6164);
#5380=PLANE('',#6165);
#5381=PLANE('',#6166);
#5382=PLANE('',#6167);
#5383=PLANE('',#6168);
#5384=PLANE('',#6169);
#5385=PLANE('',#6170);
#5626=ADVANCED_FACE('',(#812),#553,.F.);
#5627=ADVANCED_FACE('',(#813),#554,.F.);
#5628=ADVANCED_FACE('',(#814),#555,.F.);
#5629=ADVANCED_FACE('',(#815),#556,.F.);
#5630=ADVANCED_FACE('',(#816),#557,.F.);
#5631=ADVANCED_FACE('',(#817),#558,.F.);
#5632=ADVANCED_FACE('',(#818),#559,.F.);
#5633=ADVANCED_FACE('',(#819),#560,.F.);
#5634=ADVANCED_FACE('',(#820),#561,.F.);
#5635=ADVANCED_FACE('',(#821),#562,.F.);
#5636=ADVANCED_FACE('',(#822),#563,.F.);
#5637=ADVANCED_FACE('',(#823),#564,.F.);
#5638=ADVANCED_FACE('',(#824),#565,.F.);
#5639=ADVANCED_FACE('',(#825),#566,.F.);
#5640=ADVANCED_FACE('',(#826),#141,.F.);
#5641=ADVANCED_FACE('',(#827),#142,.F.);
#5642=ADVANCED_FACE('',(#828,#411),#5378,.T.);
#5643=ADVANCED_FACE('',(#829),#5379,.T.);
#5644=ADVANCED_FACE('',(#830),#5380,.T.);
#5645=ADVANCED_FACE('',(#831),#5381,.T.);
#5646=ADVANCED_FACE('',(#832),#5382,.T.);
#5647=ADVANCED_FACE('',(#833),#5383,.T.);
#5648=ADVANCED_FACE('',(#834),#5384,.T.);
#5649=ADVANCED_FACE('',(#835,#412),#5385,.F.);
#5725=CLOSED_SHELL('',(#5626,#5627,#5628,#5629,#5630,#5631,#5632,#5633,
#5634,#5635,#5636,#5637,#5638,#5639,#5640,#5641,#5642,#5643,#5644,#5645,
#5646,#5647,#5648,#5649));
#6143=AXIS2_PLACEMENT_3D('',#28593,#7104,#7105);
#6144=AXIS2_PLACEMENT_3D('',#28594,#7106,#7107);
#6145=AXIS2_PLACEMENT_3D('',#28604,#7109,#7110);
#6146=AXIS2_PLACEMENT_3D('',#28624,#7111,#7112);
#6147=AXIS2_PLACEMENT_3D('',#28760,#7114,#7115);
#6148=AXIS2_PLACEMENT_3D('',#28902,#7117,#7118);
#6149=AXIS2_PLACEMENT_3D('',#29038,#7120,#7121);
#6150=AXIS2_PLACEMENT_3D('',#29109,#7123,#7124);
#6151=AXIS2_PLACEMENT_3D('',#29127,#7126,#7127);
#6152=AXIS2_PLACEMENT_3D('',#29170,#7128,#7129);
#6153=AXIS2_PLACEMENT_3D('',#29175,#7131,#7132);
#6154=AXIS2_PLACEMENT_3D('',#29183,#7133,#7134);
#6155=AXIS2_PLACEMENT_3D('',#29267,#7136,#7137);
#6156=AXIS2_PLACEMENT_3D('',#29418,#7138,#7139);
#6157=AXIS2_PLACEMENT_3D('',#29714,#7141,#7142);
#6158=AXIS2_PLACEMENT_3D('',#30017,#7144,#7145);
#6159=AXIS2_PLACEMENT_3D('',#30190,#7147,#7148);
#6160=AXIS2_PLACEMENT_3D('',#30271,#7150,#7151);
#6161=AXIS2_PLACEMENT_3D('',#30365,#7152,#7153);
#6162=AXIS2_PLACEMENT_3D('',#30568,#7154,#7155);
#6163=AXIS2_PLACEMENT_3D('',#31129,#7156,#7157);
#6164=AXIS2_PLACEMENT_3D('',#31142,#7164,#7165);
#6165=AXIS2_PLACEMENT_3D('',#31148,#7169,#7170);
#6166=AXIS2_PLACEMENT_3D('',#31152,#7173,#7174);
#6167=AXIS2_PLACEMENT_3D('',#31156,#7177,#7178);
#6168=AXIS2_PLACEMENT_3D('',#31160,#7181,#7182);
#6169=AXIS2_PLACEMENT_3D('',#31164,#7185,#7186);
#6170=AXIS2_PLACEMENT_3D('',#31166,#7188,#7189);
#7104=DIRECTION('axis',(0.,0.,1.));
#7105=DIRECTION('refdir',(1.,0.,0.));
#7106=DIRECTION('center_axis',(0.,0.,-1.));
#7107=DIRECTION('ref_axis',(-0.609355746674506,-0.79289695042594,0.));
#7108=DIRECTION('',(0.,0.,-1.));
#7109=DIRECTION('center_axis',(0.,0.,1.));
#7110=DIRECTION('ref_axis',(1.,-3.8427904741888E-16,0.));
#7111=DIRECTION('center_axis',(0.,0.,-1.));
#7112=DIRECTION('ref_axis',(-0.609355746674506,-0.79289695042594,0.));
#7113=DIRECTION('',(0.,0.,-1.));
#7114=DIRECTION('center_axis',(0.,0.,-1.));
#7115=DIRECTION('ref_axis',(-0.609355746674506,-0.79289695042594,0.));
#7116=DIRECTION('',(0.,0.,-1.));
#7117=DIRECTION('center_axis',(0.,0.,-1.));
#7118=DIRECTION('ref_axis',(-0.609355746674506,-0.79289695042594,0.));
#7119=DIRECTION('',(0.,0.,-1.));
#7120=DIRECTION('center_axis',(0.,0.,-1.));
#7121=DIRECTION('ref_axis',(-0.609355746674506,-0.79289695042594,0.));
#7122=DIRECTION('',(0.,0.,-1.));
#7123=DIRECTION('center_axis',(0.,0.,-1.));
#7124=DIRECTION('ref_axis',(-0.609355746674506,-0.79289695042594,0.));
#7125=DIRECTION('',(0.,0.,-1.));
#7126=DIRECTION('center_axis',(0.,0.,-1.));
#7127=DIRECTION('ref_axis',(1.,-3.8427904741888E-16,0.));
#7128=DIRECTION('center_axis',(0.,0.,-1.));
#7129=DIRECTION('ref_axis',(0.938432355146259,-0.345463044064985,0.));
#7130=DIRECTION('',(0.,0.,-1.));
#7131=DIRECTION('center_axis',(0.,0.,-1.));
#7132=DIRECTION('ref_axis',(1.,0.,0.));
#7133=DIRECTION('center_axis',(0.,0.,-1.));
#7134=DIRECTION('ref_axis',(0.938432355146259,-0.345463044064985,0.));
#7135=DIRECTION('',(0.,0.,-1.));
#7136=DIRECTION('center_axis',(0.,0.,-1.));
#7137=DIRECTION('ref_axis',(1.,0.,0.));
#7138=DIRECTION('center_axis',(0.,0.,-1.));
#7139=DIRECTION('ref_axis',(0.938432355146259,-0.345463044064985,0.));
#7140=DIRECTION('',(0.,0.,-1.));
#7141=DIRECTION('center_axis',(0.,0.,-1.));
#7142=DIRECTION('ref_axis',(0.938432355146259,-0.345463044064985,0.));
#7143=DIRECTION('',(0.,0.,-1.));
#7144=DIRECTION('center_axis',(0.,0.,-1.));
#7145=DIRECTION('ref_axis',(0.938432355146259,-0.345463044064985,0.));
#7146=DIRECTION('',(0.,0.,-1.));
#7147=DIRECTION('center_axis',(0.,0.,-1.));
#7148=DIRECTION('ref_axis',(0.938432355146259,-0.345463044064985,0.));
#7149=DIRECTION('',(0.,0.,-1.));
#7150=DIRECTION('center_axis',(0.,0.,-1.));
#7151=DIRECTION('ref_axis',(1.,0.,0.));
#7152=DIRECTION('center_axis',(0.,0.,-1.));
#7153=DIRECTION('ref_axis',(0.938432355146259,-0.345463044064985,0.));
#7154=DIRECTION('center_axis',(0.,0.,-1.));
#7155=DIRECTION('ref_axis',(-0.609355746674506,-0.79289695042594,0.));
#7156=DIRECTION('center_axis',(0.,0.,1.));
#7157=DIRECTION('ref_axis',(1.,0.,0.));
#7158=DIRECTION('',(0.5,0.866025403784439,0.));
#7159=DIRECTION('',(-0.5,0.866025403784439,0.));
#7160=DIRECTION('',(-1.,1.37354477598826E-16,0.));
#7161=DIRECTION('',(-0.5,-0.866025403784439,0.));
#7162=DIRECTION('',(0.5,-0.866025403784439,0.));
#7163=DIRECTION('',(1.,-1.37354477598826E-16,0.));
#7164=DIRECTION('center_axis',(-1.37354477598826E-16,-1.,0.));
#7165=DIRECTION('ref_axis',(1.,-1.37354477598826E-16,0.));
#7166=DIRECTION('',(1.,-1.37354477598826E-16,0.));
#7167=DIRECTION('',(0.,0.,1.));
#7168=DIRECTION('',(0.,0.,1.));
#7169=DIRECTION('center_axis',(-0.866025403784439,-0.5,0.));
#7170=DIRECTION('ref_axis',(0.5,-0.866025403784439,0.));
#7171=DIRECTION('',(0.5,-0.866025403784439,0.));
#7172=DIRECTION('',(0.,0.,1.));
#7173=DIRECTION('center_axis',(-0.866025403784439,0.5,0.));
#7174=DIRECTION('ref_axis',(-0.5,-0.866025403784439,0.));
#7175=DIRECTION('',(-0.5,-0.866025403784439,0.));
#7176=DIRECTION('',(0.,0.,1.));
#7177=DIRECTION('center_axis',(1.37354477598826E-16,1.,0.));
#7178=DIRECTION('ref_axis',(-1.,1.37354477598826E-16,0.));
#7179=DIRECTION('',(-1.,1.37354477598826E-16,0.));
#7180=DIRECTION('',(0.,0.,1.));
#7181=DIRECTION('center_axis',(0.866025403784439,0.5,0.));
#7182=DIRECTION('ref_axis',(-0.5,0.866025403784439,0.));
#7183=DIRECTION('',(-0.5,0.866025403784439,0.));
#7184=DIRECTION('',(0.,0.,1.));
#7185=DIRECTION('center_axis',(0.866025403784439,-0.5,0.));
#7186=DIRECTION('ref_axis',(0.5,0.866025403784439,0.));
#7187=DIRECTION('',(0.5,0.866025403784439,0.));
#7188=DIRECTION('center_axis',(0.,0.,1.));
#7189=DIRECTION('ref_axis',(1.,0.,0.));
#28593=CARTESIAN_POINT('',(0.,0.,0.));
#28594=CARTESIAN_POINT('Origin',(0.,0.,0.554592528053768));
#28595=CARTESIAN_POINT('',(0.125207372047943,0.162920500888771,0.0106050744780265));
#28596=CARTESIAN_POINT('',(0.124934343482292,0.162564573588643,0.00478498949683932));
#28597=CARTESIAN_POINT('',(0.125207372047944,0.16292050088877,0.554592528053768));
#28598=CARTESIAN_POINT('',(0.181742788875946,0.0958620587959239,0.));
#28599=CARTESIAN_POINT('Ctrl Pts',(0.124934343482292,0.162564573588643,
0.00478498949683932));
#28600=CARTESIAN_POINT('Ctrl Pts',(0.148318591442515,0.144625169784585,
0.0031899929978929));
#28601=CARTESIAN_POINT('Ctrl Pts',(0.168018548550233,0.1218815470411,0.00159499649894647));
#28602=CARTESIAN_POINT('Ctrl Pts',(0.181742788875947,0.0958620587959227,
0.));
#28603=CARTESIAN_POINT('',(0.205337197401384,-0.00752402740192784,1.13225540054884E-10));
#28604=CARTESIAN_POINT('Origin',(0.,0.,0.));
#28605=CARTESIAN_POINT('Ctrl Pts',(0.125207372047943,0.162920500888771,
0.0106050744780265));
#28606=CARTESIAN_POINT('Ctrl Pts',(0.135191036397379,0.15524787301332,0.00991897992953218));
#28607=CARTESIAN_POINT('Ctrl Pts',(0.144499847540114,0.146628725624496,
0.00923288538103781));
#28608=CARTESIAN_POINT('Ctrl Pts',(0.152951970006133,0.137206670742508,
0.0085467908325435));
#28609=CARTESIAN_POINT('Ctrl Pts',(0.161726091348647,0.127425665656181,
0.00783455827260035));
#28610=CARTESIAN_POINT('Ctrl Pts',(0.169576008636495,0.11677979549158,0.00712232571265741));
#28611=CARTESIAN_POINT('Ctrl Pts',(0.176338684112991,0.105473428456171,
0.00641009315271424));
#28612=CARTESIAN_POINT('Ctrl Pts',(0.182841040154334,0.0946022837067508,
0.00572527695754354));
#28613=CARTESIAN_POINT('Ctrl Pts',(0.188338039031849,0.0831214749447625,
0.00504046076237263));
#28614=CARTESIAN_POINT('Ctrl Pts',(0.192729448030586,0.0712413888608711,
0.00435564456720194));
#28615=CARTESIAN_POINT('Ctrl Pts',(0.197121501740769,0.0593595586380301,
0.00367072783281035));
#28616=CARTESIAN_POINT('Ctrl Pts',(0.2004073773629,0.0470791616454508,0.00298581109841873));
#28617=CARTESIAN_POINT('Ctrl Pts',(0.202536285480387,0.034626993643793,
0.00230089436402714));
#28618=CARTESIAN_POINT('Ctrl Pts',(0.204669951533879,0.0221469960622687,
0.00161444689659701));
#28619=CARTESIAN_POINT('Ctrl Pts',(0.205641422441559,0.00949532753146084,
0.000927999429167045));
#28620=CARTESIAN_POINT('Ctrl Pts',(0.205451672523553,-0.00309610760064894,
0.000241551961736919));
#28621=CARTESIAN_POINT('Ctrl Pts',(0.205429415688848,-0.00457302781954408,
0.000161034678899832));
#28622=CARTESIAN_POINT('Ctrl Pts',(0.205391241254496,-0.00604912403675888,
8.05173960626305E-5));
#28623=CARTESIAN_POINT('Ctrl Pts',(0.205337197401384,-0.00752402740192794,
1.13225540054884E-10));
#28624=CARTESIAN_POINT('Origin',(0.,0.,0.554592528053768));
#28625=CARTESIAN_POINT('',(0.125161044493656,0.16285866358402,0.0806174252350157));
#28626=CARTESIAN_POINT('',(0.125207372047944,0.16292050088877,0.0747863044042028));
#28627=CARTESIAN_POINT('',(0.125207372047944,0.16292050088877,0.554592528053768));
#28628=CARTESIAN_POINT('',(-0.20546235540252,-0.000151937791236579,0.0295925301446521));
#28629=CARTESIAN_POINT('Ctrl Pts',(0.125207372047944,0.16292050088877,0.0747863044042028));
#28630=CARTESIAN_POINT('Ctrl Pts',(0.135260192360196,0.155194725396423,
0.0740996580920012));
#28631=CARTESIAN_POINT('Ctrl Pts',(0.144610938545834,0.146523023284227,
0.0734130117797997));
#28632=CARTESIAN_POINT('Ctrl Pts',(0.153083746180861,0.137059630381209,
0.0727263654675981));
#28633=CARTESIAN_POINT('Ctrl Pts',(0.161551511709001,0.127601869075248,
0.0720401277736786));
#28634=CARTESIAN_POINT('Ctrl Pts',(0.169141797394902,0.117353995805741,
0.071353890079759));
#28635=CARTESIAN_POINT('Ctrl Pts',(0.175717374888728,0.106505304033246,
0.0706676523858395));
#28636=CARTESIAN_POINT('Ctrl Pts',(0.182309139155736,0.0956299065739565,
0.0699797254146039));
#28637=CARTESIAN_POINT('Ctrl Pts',(0.187880772542185,0.0841514911841738,
0.0692917984433683));
#28638=CARTESIAN_POINT('Ctrl Pts',(0.192340188204511,0.0722857359819571,
0.0686038714721326));
#28639=CARTESIAN_POINT('Ctrl Pts',(0.196450264707989,0.0613495135381388,
0.0679698349313207));
#28640=CARTESIAN_POINT('Ctrl Pts',(0.199615952662604,0.0500850390171815,
0.0673357983905087));
#28641=CARTESIAN_POINT('Ctrl Pts',(0.201803192669525,0.0386710105038203,
0.0667017618496967));
#28642=CARTESIAN_POINT('Ctrl Pts',(0.204176317968265,0.0262869466882869,
0.0660138409308376));
#28643=CARTESIAN_POINT('Ctrl Pts',(0.205413490830913,0.0136405328699919,
0.0653259200119784));
#28644=CARTESIAN_POINT('Ctrl Pts',(0.205472755776309,0.000960343006070464,
0.0646379990931193));
#28645=CARTESIAN_POINT('Ctrl Pts',(0.205531897792633,-0.0116935452396088,
0.0639515050798178));
#28646=CARTESIAN_POINT('Ctrl Pts',(0.204417904171905,-0.0243802152524297,
0.0632650110665164));
#28647=CARTESIAN_POINT('Ctrl Pts',(0.202140596895965,-0.0368667154970847,
0.0625785170532149));
#28648=CARTESIAN_POINT('Ctrl Pts',(0.199863615838169,-0.0493514270841568,
0.0618921213783348));
#28649=CARTESIAN_POINT('Ctrl Pts',(0.196423760605867,-0.0616351685143203,
0.0612057257034547));
#28650=CARTESIAN_POINT('Ctrl Pts',(0.191882452794946,-0.0734921760080312,
0.0605193300285745));
#28651=CARTESIAN_POINT('Ctrl Pts',(0.187341539995639,-0.085348152156618,
0.0598329940576992));
#28652=CARTESIAN_POINT('Ctrl Pts',(0.181699696856621,-0.0967766695112979,
0.0591466580868238));
#28653=CARTESIAN_POINT('Ctrl Pts',(0.175066635828823,-0.107571597759717,
0.0584603221159485));
#28654=CARTESIAN_POINT('Ctrl Pts',(0.16841825206409,-0.118391462887969,
0.0577724006711138));
#28655=CARTESIAN_POINT('Ctrl Pts',(0.160774582289236,-0.128574111464531,
0.0570844792262791));
#28656=CARTESIAN_POINT('Ctrl Pts',(0.152288266677789,-0.137942957258697,
0.0563965577814444));
#28657=CARTESIAN_POINT('Ctrl Pts',(0.148950279128879,-0.141628077167082,
0.0561259723681009));
#28658=CARTESIAN_POINT('Ctrl Pts',(0.145482337108395,-0.145187682787088,
0.0558553869547575));
#28659=CARTESIAN_POINT('Ctrl Pts',(0.141895208834322,-0.14861266882357,
0.055584801541414));
#28660=CARTESIAN_POINT('Ctrl Pts',(0.13279099500499,-0.157305361935212,
0.0548980495565511));
#28661=CARTESIAN_POINT('Ctrl Pts',(0.122852615423652,-0.16518924674948,
0.0542112975716881));
#28662=CARTESIAN_POINT('Ctrl Pts',(0.112248597575376,-0.172105281637029,
0.0535245455868252));
#28663=CARTESIAN_POINT('Ctrl Pts',(0.101666698579554,-0.179006890412003,
0.0528392260934992));
#28664=CARTESIAN_POINT('Ctrl Pts',(0.0904225953185901,-0.184944124413337,
0.0521539066001731));
#28665=CARTESIAN_POINT('Ctrl Pts',(0.0787166429651472,-0.189799014078834,
0.0514685871068471));
#28666=CARTESIAN_POINT('Ctrl Pts',(0.0670122096419139,-0.194653273746546,
0.0507833565444327));
#28667=CARTESIAN_POINT('Ctrl Pts',(0.0548468279443643,-0.198425091847161,
0.0500981259820183));
#28668=CARTESIAN_POINT('Ctrl Pts',(0.0424428474164345,-0.201043727403233,
0.0494128954196039));
#28669=CARTESIAN_POINT('Ctrl Pts',(0.0300398755813251,-0.203662150011624,
0.0487277205802009));
#28670=CARTESIAN_POINT('Ctrl Pts',(0.0173991977050335,-0.20512742159407,
0.0480425457407979));
#28671=CARTESIAN_POINT('Ctrl Pts',(0.00475285713355531,-0.20542002330364,
0.0473573709013949));
#28672=CARTESIAN_POINT('Ctrl Pts',(-0.00792325603801462,-0.205713313869693,
0.0466705829916835));
#28673=CARTESIAN_POINT('Ctrl Pts',(-0.0206041896027675,-0.204828463813174,
0.0459837950819722));
#28674=CARTESIAN_POINT('Ctrl Pts',(-0.0330594692979208,-0.202798045145262,
0.0452970071722607));
#28675=CARTESIAN_POINT('Ctrl Pts',(-0.0380719307092315,-0.201980930197159,
0.0450206185258843));
#28676=CARTESIAN_POINT('Ctrl Pts',(-0.0430479551847099,-0.200978867605235,
0.0447442298795076));
#28677=CARTESIAN_POINT('Ctrl Pts',(-0.0479731481905962,-0.199796277937511,
0.0444678412331312));
#28678=CARTESIAN_POINT('Ctrl Pts',(-0.0602519252280685,-0.19684801685628,
0.0437787891370023));
#28679=CARTESIAN_POINT('Ctrl Pts',(-0.0723001442737591,-0.19275349126515,
0.0430897370408734));
#28680=CARTESIAN_POINT('Ctrl Pts',(-0.0838917469720236,-0.187569055057016,
0.0424006849447446));
#28681=CARTESIAN_POINT('Ctrl Pts',(-0.0954591205084849,-0.182395455533594,
0.0417130731287187));
#28682=CARTESIAN_POINT('Ctrl Pts',(-0.106570964122892,-0.176136749040885,
0.0410254613126929));
#28683=CARTESIAN_POINT('Ctrl Pts',(-0.117018611011345,-0.168898254289307,
0.040337849496667));
#28684=CARTESIAN_POINT('Ctrl Pts',(-0.127464214162663,-0.161661175510215,
0.0396503721891881));
#28685=CARTESIAN_POINT('Ctrl Pts',(-0.137245145186447,-0.153445140223816,
0.0389628948817094));
#28686=CARTESIAN_POINT('Ctrl Pts',(-0.14618056856958,-0.144399504838744,
0.0382754175742306));
#28687=CARTESIAN_POINT('Ctrl Pts',(-0.155114959869761,-0.135354914266622,
0.0375880196735777));
#28688=CARTESIAN_POINT('Ctrl Pts',(-0.163203448204579,-0.125481542661584,
0.0369006217729247));
#28689=CARTESIAN_POINT('Ctrl Pts',(-0.170302958735799,-0.1149646809713,
0.0362132238722718));
#28690=CARTESIAN_POINT('Ctrl Pts',(-0.177418338475885,-0.104424311424518,
0.0355242894627552));
#28691=CARTESIAN_POINT('Ctrl Pts',(-0.183539892256841,-0.0932383261556052,
0.0348353550532384));
#28692=CARTESIAN_POINT('Ctrl Pts',(-0.188569123495992,-0.0816190007838447,
0.0341464206437218));
#28693=CARTESIAN_POINT('Ctrl Pts',(-0.190504940680171,-0.0771465697792584,
0.0338812407374307));
#28694=CARTESIAN_POINT('Ctrl Pts',(-0.192279431480133,-0.0726101451294261,
0.0336160608311397));
#28695=CARTESIAN_POINT('Ctrl Pts',(-0.193888937113424,-0.0680224645982971,
0.0333508809248486));
#28696=CARTESIAN_POINT('Ctrl Pts',(-0.198705199436606,-0.0542943530366855,
0.0325573602529624));
#28697=CARTESIAN_POINT('Ctrl Pts',(-0.202067611815247,-0.0400300622513279,
0.031763839581076));
#28698=CARTESIAN_POINT('Ctrl Pts',(-0.203883660505739,-0.0255230994156351,
0.0309703189091898));
#28699=CARTESIAN_POINT('Ctrl Pts',(-0.204934727938483,-0.0171269609946517,
0.0305110560382134));
#28700=CARTESIAN_POINT('Ctrl Pts',(-0.205468659503104,-0.00864994056524452,
0.0300517931672369));
#28701=CARTESIAN_POINT('Ctrl Pts',(-0.205474943816094,-0.000151949903191644,
0.0295925302962604));
#28702=CARTESIAN_POINT('Ctrl Pts',(-0.205288744110104,-0.000151770750953056,
0.0295925280537678));
#28703=CARTESIAN_POINT('Ctrl Pts',(-0.204996003270372,0.0451941134373501,
0.0271396589080337));
#28704=CARTESIAN_POINT('Ctrl Pts',(-0.16789984592073,0.159522204476035,
0.0209811363262054));
#28705=CARTESIAN_POINT('Ctrl Pts',(-0.00906163169318692,0.22853860958862,
0.0127119568072292));
#28706=CARTESIAN_POINT('Ctrl Pts',(0.0939899964509164,0.186303764936298,
0.00689564643398706));
#28707=CARTESIAN_POINT('Ctrl Pts',(0.124934343482292,0.162564573588643,
0.00478498949683932));
#28708=CARTESIAN_POINT('',(-0.205474920450601,0.000180806026586553,0.0354074719462324));
#28709=CARTESIAN_POINT('Ctrl Pts',(-0.205474920450601,0.000180806026586553,
0.0354074719462324));
#28710=CARTESIAN_POINT('Ctrl Pts',(-0.205462672789408,0.0140995191186828,
0.0346517512397107));
#28711=CARTESIAN_POINT('Ctrl Pts',(-0.204034908267823,0.0279571981809514,
0.0338960305331892));
#28712=CARTESIAN_POINT('Ctrl Pts',(-0.201235673998871,0.0415232360880032,
0.0331403098266677));
#28713=CARTESIAN_POINT('Ctrl Pts',(-0.198691911824772,0.0538511696458031,
0.0324535599648376));
#28714=CARTESIAN_POINT('Ctrl Pts',(-0.195002027539007,0.0659883377117587,
0.0317668101030073));
#28715=CARTESIAN_POINT('Ctrl Pts',(-0.190214170361878,0.0777080756327314,
0.0310800602411772));
#28716=CARTESIAN_POINT('Ctrl Pts',(-0.185436300195792,0.0894033673040152,
0.0303947428737176));
#28717=CARTESIAN_POINT('Ctrl Pts',(-0.17956525817496,0.100682133855508,
0.0297094255062579));
#28718=CARTESIAN_POINT('Ctrl Pts',(-0.172698732637008,0.111333388390775,
0.0290241081387983));
#28719=CARTESIAN_POINT('Ctrl Pts',(-0.165833097875624,0.121983261166387,
0.0283388796757852));
#28720=CARTESIAN_POINT('Ctrl Pts',(-0.157972665043853,0.132005029581892,
0.0276536512127722));
#28721=CARTESIAN_POINT('Ctrl Pts',(-0.1492600756121,0.141214041275187,0.0269684227497591));
#28722=CARTESIAN_POINT('Ctrl Pts',(-0.140548194533839,0.150422304254723,
0.0262832499973907));
#28723=CARTESIAN_POINT('Ctrl Pts',(-0.130984909061376,0.15881732859402,
0.0255980772450224));
#28724=CARTESIAN_POINT('Ctrl Pts',(-0.120749968207374,0.166251077599269,
0.024912904492654));
#28725=CARTESIAN_POINT('Ctrl Pts',(-0.110490930863035,0.173702328147871,
0.0242261186133666));
#28726=CARTESIAN_POINT('Ctrl Pts',(-0.0995578191178444,0.180187324520427,
0.0235393327340791));
#28727=CARTESIAN_POINT('Ctrl Pts',(-0.0881587200673234,0.185601766427724,
0.0228525468547917));
#28728=CARTESIAN_POINT('Ctrl Pts',(-0.083571117217974,0.187780825405233,
0.0225761477426559));
#28729=CARTESIAN_POINT('Ctrl Pts',(-0.0789082812909707,0.189787029962141,
0.0222997486305201));
#28730=CARTESIAN_POINT('Ctrl Pts',(-0.0741845676270748,0.191615828028334,
0.0220233495183842));
#28731=CARTESIAN_POINT('Ctrl Pts',(-0.0624085198732363,0.196174955632579,
0.0213342965030613));
#28732=CARTESIAN_POINT('Ctrl Pts',(-0.0501701202187604,0.199660157841503,
0.0206452434877385));
#28733=CARTESIAN_POINT('Ctrl Pts',(-0.0376873519293716,0.201989205477797,
0.0199561904724155));
#28734=CARTESIAN_POINT('Ctrl Pts',(-0.0252306758224384,0.204313384808082,
0.0192685777543551));
#28735=CARTESIAN_POINT('Ctrl Pts',(-0.0125314697797735,0.205485978497169,
0.0185809650362948));
#28736=CARTESIAN_POINT('Ctrl Pts',(0.000178736612729978,0.205474922261144,
0.0178933523182345));
#28737=CARTESIAN_POINT('Ctrl Pts',(0.0128864559775172,0.205463868188512,
0.017205874146525));
#28738=CARTESIAN_POINT('Ctrl Pts',(0.0256043115927967,0.204269578020358,
0.0165183959748154));
#28739=CARTESIAN_POINT('Ctrl Pts',(0.0380986165458339,0.201912037883563,
0.0158309178031059));
#28740=CARTESIAN_POINT('Ctrl Pts',(0.0505914779703075,0.199554770124988,
0.0151435190591342));
#28741=CARTESIAN_POINT('Ctrl Pts',(0.0628599977250734,0.196034701279311,
0.0144561203151623));
#28742=CARTESIAN_POINT('Ctrl Pts',(0.0746811072610426,0.19142285089107,
0.0137687215711906));
#28743=CARTESIAN_POINT('Ctrl Pts',(0.0865286391536204,0.186800692167962,
0.0130797863644452));
#28744=CARTESIAN_POINT('Ctrl Pts',(0.0979259823920605,0.18108224616592,
0.0123908511576998));
#28745=CARTESIAN_POINT('Ctrl Pts',(0.108671384715014,0.17438608249835,0.0117019159509544));
#28746=CARTESIAN_POINT('Ctrl Pts',(0.112807358996017,0.17180868614984,0.0114367403706702));
#28747=CARTESIAN_POINT('Ctrl Pts',(0.116847046830691,0.169086900231906,
0.0111715647903859));
#28748=CARTESIAN_POINT('Ctrl Pts',(0.120780194335444,0.166229119835522,
0.0109063892101017));
#28749=CARTESIAN_POINT('Ctrl Pts',(0.122269918345648,0.165146703255102,
0.0108059509660766));
#28750=CARTESIAN_POINT('Ctrl Pts',(0.123745850864902,0.164043706535222,
0.0107055127220516));
#28751=CARTESIAN_POINT('Ctrl Pts',(0.125207372047943,0.162920500888771,
0.0106050744780265));
#28752=CARTESIAN_POINT('Ctrl Pts',(0.125161044493633,0.162858663584037,
0.0806174252350173));
#28753=CARTESIAN_POINT('Ctrl Pts',(0.139948319312594,0.151719697155996,
0.0796143338432777));
#28754=CARTESIAN_POINT('Ctrl Pts',(0.202192621330403,0.0903875593842567,
0.074905589015444));
#28755=CARTESIAN_POINT('Ctrl Pts',(0.228035008840565,-0.083631262664263,
0.0664911907515159));
#28756=CARTESIAN_POINT('Ctrl Pts',(0.0533337265757384,-0.236956827852518,
0.0553742304432329));
#28757=CARTESIAN_POINT('Ctrl Pts',(-0.154992695350211,-0.17760232906673,
0.0450130024403464));
#28758=CARTESIAN_POINT('Ctrl Pts',(-0.20504063162631,-0.0541692048004282,
0.0383574278735543));
#28759=CARTESIAN_POINT('Ctrl Pts',(-0.205542551645511,0.00018022444937596,
0.0354075067428563));
#28760=CARTESIAN_POINT('Origin',(0.,0.,0.554592528053768));
#28761=CARTESIAN_POINT('',(0.125015612364501,0.162672938451339,0.150603574429178));
#28762=CARTESIAN_POINT('',(0.125207372047945,0.162920500888769,0.144794087791587));
#28763=CARTESIAN_POINT('',(0.125207372047944,0.16292050088877,0.554592528053768));
#28764=CARTESIAN_POINT('',(-0.205474993442675,-5.19108148716082E-5,0.0995925280506006));
#28765=CARTESIAN_POINT('Ctrl Pts',(0.125207372047945,0.16292050088877,0.144794087791587));
#28766=CARTESIAN_POINT('Ctrl Pts',(0.126533996279166,0.161900966006541,
0.144702886530283));
#28767=CARTESIAN_POINT('Ctrl Pts',(0.127847586394256,0.160865672653201,
0.144611685268979));
#28768=CARTESIAN_POINT('Ctrl Pts',(0.12914775512683,0.159814996075776,0.144520484007676));
#28769=CARTESIAN_POINT('Ctrl Pts',(0.138952052153233,0.151892066546959,
0.143832754613328));
#28770=CARTESIAN_POINT('Ctrl Pts',(0.148058839276438,0.143035853394179,
0.14314502521898));
#28771=CARTESIAN_POINT('Ctrl Pts',(0.156288532458628,0.133393666442333,
0.142457295824632));
#28772=CARTESIAN_POINT('Ctrl Pts',(0.164501105837628,0.123771537631085,
0.141770997078015));
#28773=CARTESIAN_POINT('Ctrl Pts',(0.171839594963137,0.113367283593476,
0.141084698331399));
#28774=CARTESIAN_POINT('Ctrl Pts',(0.17816111201773,0.102365002757808,0.140398399584782));
#28775=CARTESIAN_POINT('Ctrl Pts',(0.184481700913311,0.0913643373359736,
0.139712201604225));
#28776=CARTESIAN_POINT('Ctrl Pts',(0.189785143090681,0.079766544590134,
0.139026003623668));
#28777=CARTESIAN_POINT('Ctrl Pts',(0.193972586509944,0.0677835622230219,
0.138339805643111));
#28778=CARTESIAN_POINT('Ctrl Pts',(0.198159655731775,0.0558016506766435,
0.137653668982433));
#28779=CARTESIAN_POINT('Ctrl Pts',(0.201230661855283,0.0434354425276815,
0.136967532321755));
#28780=CARTESIAN_POINT('Ctrl Pts',(0.203136303503206,0.0309130688229653,
0.136281395661077));
#28781=CARTESIAN_POINT('Ctrl Pts',(0.205046352401837,0.0183617341431124,
0.135593672145762));
#28782=CARTESIAN_POINT('Ctrl Pts',(0.205785584821844,0.00565437702989593,
0.134905948630448));
#28783=CARTESIAN_POINT('Ctrl Pts',(0.205356555857814,-0.00697571438753253,
0.134218225115133));
#28784=CARTESIAN_POINT('Ctrl Pts',(0.205187141601162,-0.0119630642597618,
0.133946657976553));
#28785=CARTESIAN_POINT('Ctrl Pts',(0.204836135880033,-0.01693839824953,
0.133675090837974));
#28786=CARTESIAN_POINT('Ctrl Pts',(0.204305913300231,-0.0218876544097049,
0.133403523699394));
#28787=CARTESIAN_POINT('Ctrl Pts',(0.202963143048502,-0.034421473589077,
0.13271578936117));
#28788=CARTESIAN_POINT('Ctrl Pts',(0.200457982603897,-0.0468750981425169,
0.132028055022946));
#28789=CARTESIAN_POINT('Ctrl Pts',(0.196816867803737,-0.0590177615038569,
0.131340320684722));
#28790=CARTESIAN_POINT('Ctrl Pts',(0.193183326817346,-0.0711351671416734,
0.130654016889637));
#28791=CARTESIAN_POINT('Ctrl Pts',(0.188418696734644,-0.0829420542843885,
0.129967713094553));
#28792=CARTESIAN_POINT('Ctrl Pts',(0.182600220325673,-0.0942185499889263,
0.129281409299469));
#28793=CARTESIAN_POINT('Ctrl Pts',(0.176782597581181,-0.105493391249386,
0.128595206196238));
#28794=CARTESIAN_POINT('Ctrl Pts',(0.169911789447793,-0.116237206609658,
0.127909003093007));
#28795=CARTESIAN_POINT('Ctrl Pts',(0.162112304146814,-0.126252035505219,
0.127222799989776));
#28796=CARTESIAN_POINT('Ctrl Pts',(0.154313515265857,-0.136265970171596,
0.126536658157971));
#28797=CARTESIAN_POINT('Ctrl Pts',(0.145586764616251,-0.145550380111688,
0.125850516326165));
#28798=CARTESIAN_POINT('Ctrl Pts',(0.136097029331549,-0.15394016445401,
0.12516437449436));
#28799=CARTESIAN_POINT('Ctrl Pts',(0.126585347297815,-0.162349351707568,
0.124476645834035));
#28800=CARTESIAN_POINT('Ctrl Pts',(0.1163078453797,-0.169859254438693,0.123788917173711));
#28801=CARTESIAN_POINT('Ctrl Pts',(0.1054619457945,-0.176345551727958,0.123101188513387));
#28802=CARTESIAN_POINT('Ctrl Pts',(0.101179567784339,-0.178906591193676,
0.122829646805962));
#28803=CARTESIAN_POINT('Ctrl Pts',(0.0968088623768857,-0.181308553120973,
0.122558105098536));
#28804=CARTESIAN_POINT('Ctrl Pts',(0.0923629294268599,-0.183545811427798,
0.122286563391111));
#28805=CARTESIAN_POINT('Ctrl Pts',(0.0811031496119801,-0.189211896860714,
0.121598856250555));
#28806=CARTESIAN_POINT('Ctrl Pts',(0.0692806436434433,-0.193857829957916,
0.120911149109999));
#28807=CARTESIAN_POINT('Ctrl Pts',(0.0571036400178444,-0.197380723277914,
0.120223441969443));
#28808=CARTESIAN_POINT('Ctrl Pts',(0.0449519676547056,-0.200896288084425,
0.119537165434527));
#28809=CARTESIAN_POINT('Ctrl Pts',(0.0324480632690806,-0.203293141389066,
0.118850888899612));
#28810=CARTESIAN_POINT('Ctrl Pts',(0.0198185460416459,-0.204516994056228,
0.118164612364696));
#28811=CARTESIAN_POINT('Ctrl Pts',(0.00719087598648223,-0.205740667724726,
0.11747843620345));
#28812=CARTESIAN_POINT('Ctrl Pts',(-0.00556151550682495,-0.205791551073304,
0.116792260042204));
#28813=CARTESIAN_POINT('Ctrl Pts',(-0.0182047982369213,-0.204666951279763,
0.116106083880958));
#28814=CARTESIAN_POINT('Ctrl Pts',(-0.03084695479573,-0.203542451657359,
0.115419968839272));
#28815=CARTESIAN_POINT('Ctrl Pts',(-0.0433791623346208,-0.201242777741841,
0.114733853797587));
#28816=CARTESIAN_POINT('Ctrl Pts',(-0.0555732645159496,-0.197817056635772,
0.114047738755902));
#28817=CARTESIAN_POINT('Ctrl Pts',(-0.0677955817975969,-0.194383408987574,
0.113360036159476));
#28818=CARTESIAN_POINT('Ctrl Pts',(-0.079677415121298,-0.189818803845433,
0.11267233356305));
#28819=CARTESIAN_POINT('Ctrl Pts',(-0.0910072878395048,-0.184221739176183,
0.111984630966624));
#28820=CARTESIAN_POINT('Ctrl Pts',(-0.0954831384146339,-0.18201062650599,
0.111712955005358));
#28821=CARTESIAN_POINT('Ctrl Pts',(-0.0998731142906491,-0.179638895026068,
0.111441279044093));
#28822=CARTESIAN_POINT('Ctrl Pts',(-0.10416536863244,-0.177114515505274,
0.111169603082828));
#28823=CARTESIAN_POINT('Ctrl Pts',(-0.115031174605359,-0.170724069858124,
0.110481857658734));
#28824=CARTESIAN_POINT('Ctrl Pts',(-0.125344713458378,-0.163307637310166,
0.10979411223464));
#28825=CARTESIAN_POINT('Ctrl Pts',(-0.134906633517487,-0.154984437470278,
0.109106366810546));
#28826=CARTESIAN_POINT('Ctrl Pts',(-0.144448659959639,-0.146678554084455,
0.108420052243847));
#28827=CARTESIAN_POINT('Ctrl Pts',(-0.153241477344281,-0.137470154345247,
0.107733737677149));
#28828=CARTESIAN_POINT('Ctrl Pts',(-0.161116603529287,-0.127520256007376,
0.10704742311045));
#28829=CARTESIAN_POINT('Ctrl Pts',(-0.168990567313194,-0.117571826315528,
0.106361209846612));
#28830=CARTESIAN_POINT('Ctrl Pts',(-0.17594653596607,-0.106882763030196,
0.105674996582773));
#28831=CARTESIAN_POINT('Ctrl Pts',(-0.181855475767578,-0.0956481131980548,
0.104988783318935));
#28832=CARTESIAN_POINT('Ctrl Pts',(-0.187763885043637,-0.084414472052386,
0.104302631665743));
#28833=CARTESIAN_POINT('Ctrl Pts',(-0.192625071016067,-0.0726361185384288,
0.103616480012551));
#28834=CARTESIAN_POINT('Ctrl Pts',(-0.196356620124702,-0.0605314245512496,
0.102930328359358));
#28835=CARTESIAN_POINT('Ctrl Pts',(-0.200096795289964,-0.0483987486796708,
0.102242590559812));
#28836=CARTESIAN_POINT('Ctrl Pts',(-0.20270192231038,-0.0359390704211971,
0.101554852760265));
#28837=CARTESIAN_POINT('Ctrl Pts',(-0.204140116154794,-0.0233835113126177,
0.100867114960718));
#28838=CARTESIAN_POINT('Ctrl Pts',(-0.204707856207942,-0.0184270905746907,
0.100595624231994));
#28839=CARTESIAN_POINT('Ctrl Pts',(-0.205094320000884,-0.0134557812286958,
0.10032413350327));
#28840=CARTESIAN_POINT('Ctrl Pts',(-0.205299781453641,-0.00848382932921304,
0.100052642774545));
#28841=CARTESIAN_POINT('Ctrl Pts',(-0.205415851517875,-0.0056750553786874,
0.0998992712009528));
#28842=CARTESIAN_POINT('Ctrl Pts',(-0.205474283030533,-0.00286388298952928,
0.0997458996273603));
#28843=CARTESIAN_POINT('Ctrl Pts',(-0.20547499344266,-5.19108729419778E-5,
0.0995925280537679));
#28844=CARTESIAN_POINT('Ctrl Pts',(-0.205474993442675,-5.19108148716082E-5,
0.0995925280506004));
#28845=CARTESIAN_POINT('Ctrl Pts',(-0.205478158112058,0.0124745814452694,
0.0989093036977783));
#28846=CARTESIAN_POINT('Ctrl Pts',(-0.204331518578654,0.0250472595540262,
0.0982260793449564));
#28847=CARTESIAN_POINT('Ctrl Pts',(-0.202035879687132,0.0374363318722169,
0.0975428549921343));
#28848=CARTESIAN_POINT('Ctrl Pts',(-0.199625866061445,0.0504426601787855,
0.0968255906149783));
#28849=CARTESIAN_POINT('Ctrl Pts',(-0.195949068210376,0.0632455487890031,
0.0961083262378224));
#28850=CARTESIAN_POINT('Ctrl Pts',(-0.191068136702914,0.0755840112846409,
0.0953910618606664));
#28851=CARTESIAN_POINT('Ctrl Pts',(-0.18642882519258,0.0873116847806354,
0.0947093041109819));
#28852=CARTESIAN_POINT('Ctrl Pts',(-0.180702384870152,0.0986190302533711,
0.0940275463612974));
#28853=CARTESIAN_POINT('Ctrl Pts',(-0.173993039971578,0.109299577613315,
0.093345788611613));
#28854=CARTESIAN_POINT('Ctrl Pts',(-0.167283223855812,0.119980875099776,
0.0926639829800598));
#28855=CARTESIAN_POINT('Ctrl Pts',(-0.159590862137391,0.130034563297859,
0.0919821773485063));
#28856=CARTESIAN_POINT('Ctrl Pts',(-0.151063415701073,0.13928323682958,
0.0913003717169531));
#28857=CARTESIAN_POINT('Ctrl Pts',(-0.142516961859761,0.148552525358391,
0.0906170463624837));
#28858=CARTESIAN_POINT('Ctrl Pts',(-0.133132359550586,0.157012629513546,
0.0899337210080143));
#28859=CARTESIAN_POINT('Ctrl Pts',(-0.123092726545284,0.164524029541729,
0.0892503956535449));
#28860=CARTESIAN_POINT('Ctrl Pts',(-0.121551437864583,0.165677182832646,
0.0891454912577842));
#28861=CARTESIAN_POINT('Ctrl Pts',(-0.119994765657942,0.166808060439192,
0.0890405868620236));
#28862=CARTESIAN_POINT('Ctrl Pts',(-0.118423428086134,0.167916250867295,
0.088935682466263));
#28863=CARTESIAN_POINT('Ctrl Pts',(-0.108124263520439,0.175179766864068,
0.088248097790005));
#28864=CARTESIAN_POINT('Ctrl Pts',(-0.0971182332163936,0.181517662625345,
0.087560513113747));
#28865=CARTESIAN_POINT('Ctrl Pts',(-0.0855960337030366,0.186797469574158,
0.086872928437489));
#28866=CARTESIAN_POINT('Ctrl Pts',(-0.0740978098127389,0.192066290195137,
0.0861867745011692));
#28867=CARTESIAN_POINT('Ctrl Pts',(-0.0620862963673555,0.196280968083181,
0.0855006205648494));
#28868=CARTESIAN_POINT('Ctrl Pts',(-0.0497775549847631,0.199354384563618,
0.0848144666285295));
#28869=CARTESIAN_POINT('Ctrl Pts',(-0.0374705848010918,0.202427358786656,
0.0841284114281465));
#28870=CARTESIAN_POINT('Ctrl Pts',(-0.024867298253071,0.204359142474981,
0.0834423562277635));
#28871=CARTESIAN_POINT('Ctrl Pts',(-0.0121985044514171,0.205112583997542,
0.0827563010273805));
#28872=CARTESIAN_POINT('Ctrl Pts',(0.000469175482691606,0.205865959275907,
0.0820703061464434));
#28873=CARTESIAN_POINT('Ctrl Pts',(0.0132014858459238,0.205441171173303,
0.0813843112655062));
#28874=CARTESIAN_POINT('Ctrl Pts',(0.0257655867619812,0.20385315833661,
0.080698316384569));
#28875=CARTESIAN_POINT('Ctrl Pts',(0.0383588268137166,0.202261462520783,
0.0800107305184875));
#28876=CARTESIAN_POINT('Ctrl Pts',(0.0507822274498415,0.199501323851069,
0.0793231446524059));
#28877=CARTESIAN_POINT('Ctrl Pts',(0.0628121673557659,0.195638971723609,
0.0786355587863244));
#28878=CARTESIAN_POINT('Ctrl Pts',(0.0675759338595545,0.194109509080029,
0.0783632799102093));
#28879=CARTESIAN_POINT('Ctrl Pts',(0.0722781904676448,0.192407754399022,
0.0780910010340942));
#28880=CARTESIAN_POINT('Ctrl Pts',(0.0769059571795283,0.190539889197251,
0.0778187221579791));
#28881=CARTESIAN_POINT('Ctrl Pts',(0.0885973767354331,0.185820983274074,
0.0771308468230583));
#28882=CARTESIAN_POINT('Ctrl Pts',(0.0998936717960377,0.180005521932965,
0.0764429714881376));
#28883=CARTESIAN_POINT('Ctrl Pts',(0.110580041473782,0.173182071972409,
0.0757550961532168));
#28884=CARTESIAN_POINT('Ctrl Pts',(0.115596874343119,0.169978728921711,
0.0754321655702121));
#28885=CARTESIAN_POINT('Ctrl Pts',(0.120479518615123,0.166553942355756,
0.0751092349872075));
#28886=CARTESIAN_POINT('Ctrl Pts',(0.125207372047944,0.16292050088877,0.0747863044042028));
#28887=CARTESIAN_POINT('',(-0.205137705209698,-7.29564938455052E-7,0.105407471946233));
#28888=CARTESIAN_POINT('Ctrl Pts',(-0.205137705209698,-7.29564938455052E-7,
0.105407471946233));
#28889=CARTESIAN_POINT('Ctrl Pts',(-0.205136713680842,0.0343461846931921,
0.103552338522943));
#28890=CARTESIAN_POINT('Ctrl Pts',(-0.180678665067047,0.137302931168816,
0.0979915516635594));
#28891=CARTESIAN_POINT('Ctrl Pts',(-0.0354393139172565,0.230872355804693,
0.0897282027598211));
#28892=CARTESIAN_POINT('Ctrl Pts',(0.0853206790052409,0.192869635794213,
0.0833199872793719));
#28893=CARTESIAN_POINT('Ctrl Pts',(0.125161044493633,0.162858663584037,
0.0806174252350173));
#28894=CARTESIAN_POINT('Ctrl Pts',(0.125015612364502,0.162672938451338,
0.150603574429178));
#28895=CARTESIAN_POINT('Ctrl Pts',(0.155720339957463,0.138903214455256,
0.14850568725595));
#28896=CARTESIAN_POINT('Ctrl Pts',(0.223157023264117,0.0501045043133742,
0.142702146646629));
#28897=CARTESIAN_POINT('Ctrl Pts',(0.193712423773769,-0.146520715699965,
0.133192952601213));
#28898=CARTESIAN_POINT('Ctrl Pts',(-0.0181106010581924,-0.24220824221319,
0.12207599229293));
#28899=CARTESIAN_POINT('Ctrl Pts',(-0.18076764144762,-0.137130727182572,
0.112814165407936));
#28900=CARTESIAN_POINT('Ctrl Pts',(-0.205138694272785,-0.0342622287190314,
0.107257991959037));
#28901=CARTESIAN_POINT('Ctrl Pts',(-0.205137705209698,-7.29564938455052E-7,
0.105407471946233));
#28902=CARTESIAN_POINT('Origin',(0.,0.,0.554592528053768));
#28903=CARTESIAN_POINT('',(0.125207372047944,0.16292050088877,0.220601534780829));
#28904=CARTESIAN_POINT('',(0.125103714720563,0.162782948353132,0.214801399208945));
#28905=CARTESIAN_POINT('',(0.125207372047944,0.16292050088877,0.554592528053768));
#28906=CARTESIAN_POINT('',(-0.205474914417448,0.000187537043271921,0.16959252654344));
#28907=CARTESIAN_POINT('Ctrl Pts',(0.125103714720543,0.162782948353147,
0.214801399208946));
#28908=CARTESIAN_POINT('Ctrl Pts',(0.142694629810408,0.149496203490235,
0.213608348091755));
#28909=CARTESIAN_POINT('Ctrl Pts',(0.206176667207859,0.0838646344828523,
0.20870964353847));
#28910=CARTESIAN_POINT('Ctrl Pts',(0.223448082612567,-0.0952038262864637,
0.20010528554909));
#28911=CARTESIAN_POINT('Ctrl Pts',(0.0411315804786337,-0.23937629702844,
0.188988325240808));
#28912=CARTESIAN_POINT('Ctrl Pts',(-0.160132400758511,-0.170716737438922,
0.1788174060757));
#28913=CARTESIAN_POINT('Ctrl Pts',(-0.204971567375627,-0.0507230854143627,
0.172352140346687));
#28914=CARTESIAN_POINT('Ctrl Pts',(-0.205429022845128,0.000187467295045865,
0.169592528053768));
#28915=CARTESIAN_POINT('Ctrl Pts',(-0.205474914417448,0.000187537043271921,
0.16959252654344));
#28916=CARTESIAN_POINT('Ctrl Pts',(-0.20546003488534,0.0164902926646276,
0.168709023204908));
#28917=CARTESIAN_POINT('Ctrl Pts',(-0.203501056447997,0.0327051355942583,
0.167825519866375));
#28918=CARTESIAN_POINT('Ctrl Pts',(-0.199682357505078,0.048445141409787,
0.166942016527842));
#28919=CARTESIAN_POINT('Ctrl Pts',(-0.199412057308611,0.0495592713079335,
0.166879479226642));
#28920=CARTESIAN_POINT('Ctrl Pts',(-0.199132458627398,0.0506710315391687,
0.166816941925442));
#28921=CARTESIAN_POINT('Ctrl Pts',(-0.19884360010305,0.0517802889433662,
0.166754404624242));
#28922=CARTESIAN_POINT('Ctrl Pts',(-0.195666995000812,0.0639788997955671,
0.166066675880494));
#28923=CARTESIAN_POINT('Ctrl Pts',(-0.191352556686954,0.0759267682013015,
0.165378947136745));
#28924=CARTESIAN_POINT('Ctrl Pts',(-0.185960463086372,0.0873995525944041,
0.164691218392996));
#28925=CARTESIAN_POINT('Ctrl Pts',(-0.180579586019762,0.0988484715123463,
0.164004920249936));
#28926=CARTESIAN_POINT('Ctrl Pts',(-0.174125800579575,0.109823461849753,
0.163318622106875));
#28927=CARTESIAN_POINT('Ctrl Pts',(-0.166707929573821,0.120118449216638,
0.162632323963815));
#28928=CARTESIAN_POINT('Ctrl Pts',(-0.159291146875126,0.130411926162617,
0.161946126510442));
#28929=CARTESIAN_POINT('Ctrl Pts',(-0.150911025889177,0.140024870067992,
0.16125992905707));
#28930=CARTESIAN_POINT('Ctrl Pts',(-0.141719906483916,0.148779849882939,
0.160573731603697));
#28931=CARTESIAN_POINT('Ctrl Pts',(-0.132529607834903,0.157534047888397,
0.159887595426957));
#28932=CARTESIAN_POINT('Ctrl Pts',(-0.12252909774965,0.165429854936943,
0.159201459250217));
#28933=CARTESIAN_POINT('Ctrl Pts',(-0.111905896277347,0.172328308769522,
0.158515323073477));
#28934=CARTESIAN_POINT('Ctrl Pts',(-0.101258124978244,0.179242717662003,
0.157827599969569));
#28935=CARTESIAN_POINT('Ctrl Pts',(-0.0899855450072962,0.185154746955193,
0.157139876865662));
#28936=CARTESIAN_POINT('Ctrl Pts',(-0.0783017522917341,0.189970553541974,
0.156452153761754));
#28937=CARTESIAN_POINT('Ctrl Pts',(-0.0736880270710313,0.191872231263273,
0.156180583946489));
#28938=CARTESIAN_POINT('Ctrl Pts',(-0.0690103880702461,0.193603509023575,
0.155909014131224));
#28939=CARTESIAN_POINT('Ctrl Pts',(-0.0642826260963226,0.195160753245012,
0.155637444315959));
#28940=CARTESIAN_POINT('Ctrl Pts',(-0.0523099317195422,0.199104354728359,
0.154949714599857));
#28941=CARTESIAN_POINT('Ctrl Pts',(-0.0399311091990029,0.201955891739313,
0.154261984883755));
#28942=CARTESIAN_POINT('Ctrl Pts',(-0.0273673002084757,0.2036443137048,
0.153574255167652));
#28943=CARTESIAN_POINT('Ctrl Pts',(-0.0148297791737362,0.205329202891175,
0.152887964426656));
#28944=CARTESIAN_POINT('Ctrl Pts',(-0.00210887860604118,0.20585562065462,
0.152201673685659));
#28945=CARTESIAN_POINT('Ctrl Pts',(0.0105632472606296,0.205203297810515,
0.151515382944663));
#28946=CARTESIAN_POINT('Ctrl Pts',(0.023232324583079,0.204551131896278,
0.15082925730522));
#28947=CARTESIAN_POINT('Ctrl Pts',(0.0358517861306209,0.202720787990091,
0.150143131665778));
#28948=CARTESIAN_POINT('Ctrl Pts',(0.0481900208858049,0.199744080042503,
0.149457006026335));
#28949=CARTESIAN_POINT('Ctrl Pts',(0.060527095013038,0.196767652106643,
0.148770944929075));
#28950=CARTESIAN_POINT('Ctrl Pts',(0.072582160107258,0.192645300831173,
0.148084883831814));
#28951=CARTESIAN_POINT('Ctrl Pts',(0.084136856198351,0.187459235712882,
0.147398822734554));
#28952=CARTESIAN_POINT('Ctrl Pts',(0.0957157812287071,0.182262295980861,
0.146711323041893));
#28953=CARTESIAN_POINT('Ctrl Pts',(0.106791480451592,0.175997600872094,
0.146023823349231));
#28954=CARTESIAN_POINT('Ctrl Pts',(0.117169482386542,0.168793625538021,
0.14533632365657));
#28955=CARTESIAN_POINT('Ctrl Pts',(0.119897883536421,0.166899683456647,
0.145155578368242));
#28956=CARTESIAN_POINT('Ctrl Pts',(0.122578229909477,0.164941044504228,
0.144974833079914));
#28957=CARTESIAN_POINT('Ctrl Pts',(0.125207372047945,0.16292050088877,0.144794087791587));
#28958=CARTESIAN_POINT('',(-0.205474918801311,-0.000182670727437368,0.175407471946233));
#28959=CARTESIAN_POINT('Ctrl Pts',(-0.205537738049557,-0.000182131345404107,
0.175407439637765));
#28960=CARTESIAN_POINT('Ctrl Pts',(-0.205035768459691,0.0542506832901805,
0.172452904267196));
#28961=CARTESIAN_POINT('Ctrl Pts',(-0.154875619861323,0.177771679933206,
0.165792715460535));
#28962=CARTESIAN_POINT('Ctrl Pts',(0.0114351922188548,0.224924155783168,
0.157524760391006));
#28963=CARTESIAN_POINT('Ctrl Pts',(0.101484306313129,0.180889437797084,
0.152211340692044));
#28964=CARTESIAN_POINT('Ctrl Pts',(0.125015612364502,0.162672938451338,
0.150603574429178));
#28965=CARTESIAN_POINT('Ctrl Pts',(0.125207372047944,0.16292050088877,0.220601534780829));
#28966=CARTESIAN_POINT('Ctrl Pts',(0.135229999383183,0.155217929249134,
0.219914936476142));
#28967=CARTESIAN_POINT('Ctrl Pts',(0.144564381930118,0.146567701750036,
0.219228338171454));
#28968=CARTESIAN_POINT('Ctrl Pts',(0.153031143228616,0.137118360649268,
0.218541739866767));
#28969=CARTESIAN_POINT('Ctrl Pts',(0.161494455183014,0.127672869193935,
0.217855421281057));
#28970=CARTESIAN_POINT('Ctrl Pts',(0.169090227725395,0.117429513005291,
0.217169102695347));
#28971=CARTESIAN_POINT('Ctrl Pts',(0.17567590576567,0.106573691680506,0.216482784109637));
#28972=CARTESIAN_POINT('Ctrl Pts',(0.182259370136659,0.0957215193646887,
0.215796696218832));
#28973=CARTESIAN_POINT('Ctrl Pts',(0.187832975118639,0.0842580367541301,
0.215110608328027));
#28974=CARTESIAN_POINT('Ctrl Pts',(0.192298948011159,0.0723953742914676,
0.214424520437223));
#28975=CARTESIAN_POINT('Ctrl Pts',(0.196775565953506,0.0605044361011993,
0.213736797193952));
#28976=CARTESIAN_POINT('Ctrl Pts',(0.200139011911504,0.0482132446836958,
0.213049073950681));
#28977=CARTESIAN_POINT('Ctrl Pts',(0.202340970147259,0.0357506283142815,
0.21236135070741));
#28978=CARTESIAN_POINT('Ctrl Pts',(0.203781438193507,0.027597884832918,
0.211911458724671));
#28979=CARTESIAN_POINT('Ctrl Pts',(0.204725906820054,0.0193720658313528,
0.211461566741931));
#28980=CARTESIAN_POINT('Ctrl Pts',(0.205172899463256,0.0111380856003394,
0.211011674759192));
#28981=CARTESIAN_POINT('Ctrl Pts',(0.205856195198212,-0.00144879621779465,
0.210323946946057));
#28982=CARTESIAN_POINT('Ctrl Pts',(0.205379296652322,-0.0141428135166041,
0.209636219132922));
#28983=CARTESIAN_POINT('Ctrl Pts',(0.203731311683629,-0.0267119498477401,
0.208948491319788));
#28984=CARTESIAN_POINT('Ctrl Pts',(0.202086754839864,-0.0392549399637114,
0.208262194112456));
#28985=CARTESIAN_POINT('Ctrl Pts',(0.199275985054326,-0.0516727063359742,
0.207575896905125));
#28986=CARTESIAN_POINT('Ctrl Pts',(0.195340006274478,-0.0637358421430748,
0.206889599697793));
#28987=CARTESIAN_POINT('Ctrl Pts',(0.191404604920815,-0.075797208232684,
0.206203403173418));
#28988=CARTESIAN_POINT('Ctrl Pts',(0.186344545251388,-0.0875032115397956,
0.205517206649042));
#28989=CARTESIAN_POINT('Ctrl Pts',(0.180250997610476,-0.0986384990023071,
0.204831010124667));
#28990=CARTESIAN_POINT('Ctrl Pts',(0.17415799409207,-0.109772792140843,
0.204144874874117));
#28991=CARTESIAN_POINT('Ctrl Pts',(0.167032122503542,-0.120335723462707,
0.203458739623567));
#28992=CARTESIAN_POINT('Ctrl Pts',(0.15900976532022,-0.130137889017029,
0.202772604373016));
#28993=CARTESIAN_POINT('Ctrl Pts',(0.150968853384569,-0.139962725807498,
0.202084882173724));
#28994=CARTESIAN_POINT('Ctrl Pts',(0.142027910315271,-0.149022652279799,
0.201397159974432));
#28995=CARTESIAN_POINT('Ctrl Pts',(0.13236187985571,-0.157163317558718,
0.20070943777514));
#28996=CARTESIAN_POINT('Ctrl Pts',(0.128544863587495,-0.16037798276526,
0.20043786333373));
#28997=CARTESIAN_POINT('Ctrl Pts',(0.12461513953985,-0.163449748249725,
0.200166288892319));
#28998=CARTESIAN_POINT('Ctrl Pts',(0.120584741148151,-0.166370958485048,
0.199894714450909));
#28999=CARTESIAN_POINT('Ctrl Pts',(0.110378272528381,-0.173768549914217,
0.19920698690023));
#29000=CARTESIAN_POINT('Ctrl Pts',(0.0994528298630109,-0.180249297313827,
0.19851925934955));
#29001=CARTESIAN_POINT('Ctrl Pts',(0.0879974741651207,-0.185678270579944,
0.19783153179887));
#29002=CARTESIAN_POINT('Ctrl Pts',(0.076565947853254,-0.191095950517152,
0.197145234856346));
#29003=CARTESIAN_POINT('Ctrl Pts',(0.0646074384906068,-0.195465765742606,
0.196458937913822));
#29004=CARTESIAN_POINT('Ctrl Pts',(0.0523369473541958,-0.198697809667455,
0.195772640971298));
#29005=CARTESIAN_POINT('Ctrl Pts',(0.0400682563455929,-0.201929379439144,
0.19508644471115));
#29006=CARTESIAN_POINT('Ctrl Pts',(0.0274884973790633,-0.204023243709893,
0.194400248451003));
#29007=CARTESIAN_POINT('Ctrl Pts',(0.0148280576884289,-0.204939269858631,
0.193714052190855));
#29008=CARTESIAN_POINT('Ctrl Pts',(0.0021687485099159,-0.205855214210946,
0.193027917204503));
#29009=CARTESIAN_POINT('Ctrl Pts',(-0.0105703625229801,-0.20559349116586,
0.192341782218151));
#29010=CARTESIAN_POINT('Ctrl Pts',(-0.0231561837545491,-0.204166027484804,
0.191655647231799));
#29011=CARTESIAN_POINT('Ctrl Pts',(-0.0357711145876626,-0.202735262239375,
0.190967925291708));
#29012=CARTESIAN_POINT('Ctrl Pts',(-0.0482311949624943,-0.200133530206466,
0.190280203351617));
#29013=CARTESIAN_POINT('Ctrl Pts',(-0.0603118844336391,-0.196424164045729,
0.189592481411526));
#29014=CARTESIAN_POINT('Ctrl Pts',(-0.0650824496700984,-0.194959365757686,
0.189320905655226));
#29015=CARTESIAN_POINT('Ctrl Pts',(-0.0697940336714093,-0.193322389566768,
0.189049329898927));
#29016=CARTESIAN_POINT('Ctrl Pts',(-0.0744336798374629,-0.191519197290648,
0.188777754142627));
#29017=CARTESIAN_POINT('Ctrl Pts',(-0.0861829337940887,-0.186952865457034,
0.188090026584311));
#29018=CARTESIAN_POINT('Ctrl Pts',(-0.0975515135574834,-0.181285346209476,
0.187402299025996));
#29019=CARTESIAN_POINT('Ctrl Pts',(-0.108323544963334,-0.174602363190126,
0.18671457146768));
#29020=CARTESIAN_POINT('Ctrl Pts',(-0.119073168379992,-0.167933282117922,
0.186028274520835));
#29021=CARTESIAN_POINT('Ctrl Pts',(-0.129227940214968,-0.160253318696065,
0.185341977573991));
#29022=CARTESIAN_POINT('Ctrl Pts',(-0.13859575768312,-0.151694401931126,
0.184655680627146));
#29023=CARTESIAN_POINT('Ctrl Pts',(-0.147962200789884,-0.143136740852985,
0.183969484367577));
#29024=CARTESIAN_POINT('Ctrl Pts',(-0.156541249448778,-0.133700930003651,
0.183283288108009));
#29025=CARTESIAN_POINT('Ctrl Pts',(-0.16417428565667,-0.123558810103214,
0.18259709184844));
#29026=CARTESIAN_POINT('Ctrl Pts',(-0.171806640242344,-0.113417595883566,
0.181910956865486));
#29027=CARTESIAN_POINT('Ctrl Pts',(-0.178492649406469,-0.102570903692749,
0.181224821882532));
#29028=CARTESIAN_POINT('Ctrl Pts',(-0.184115975112121,-0.091221068473861,
0.180538686899578));
#29029=CARTESIAN_POINT('Ctrl Pts',(-0.189752306909373,-0.0798449824197511,
0.179850964967031));
#29030=CARTESIAN_POINT('Ctrl Pts',(-0.194320717629835,-0.0679642316562059,
0.179163243034484));
#29031=CARTESIAN_POINT('Ctrl Pts',(-0.197752701812011,-0.0558018328646087,
0.178475521101937));
#29032=CARTESIAN_POINT('Ctrl Pts',(-0.199107964243351,-0.0509990012423567,
0.178203945346073));
#29033=CARTESIAN_POINT('Ctrl Pts',(-0.200286569711164,-0.0461523936391531,
0.177932369590209));
#29034=CARTESIAN_POINT('Ctrl Pts',(-0.201286504152218,-0.0412761295566736,
0.177660793834344));
#29035=CARTESIAN_POINT('Ctrl Pts',(-0.20405206049521,-0.0277896623346762,
0.176909686538307));
#29036=CARTESIAN_POINT('Ctrl Pts',(-0.205462620446207,-0.0140163240550913,
0.17615857924227));
#29037=CARTESIAN_POINT('Ctrl Pts',(-0.205474918801311,-0.000182670727437368,
0.175407471946233));
#29038=CARTESIAN_POINT('Origin',(0.,0.,0.554592528053768));
#29039=CARTESIAN_POINT('',(0.12529644997826,0.163038483752229,0.290616425505885));
#29040=CARTESIAN_POINT('',(0.125045885691725,0.162713195961813,0.284785992558171));
#29041=CARTESIAN_POINT('',(0.125207372047944,0.16292050088877,0.554592528053768));
#29042=CARTESIAN_POINT('',(-0.205152667291151,-5.77023530759641E-5,0.239592528053768));
#29043=CARTESIAN_POINT('Ctrl Pts',(0.125045885691731,0.162713195961808,
0.284785992558171));
#29044=CARTESIAN_POINT('Ctrl Pts',(0.158439081624707,0.136730312047757,
0.282498664274471));
#29045=CARTESIAN_POINT('Ctrl Pts',(0.22621726887686,0.0424891423794237,
0.276505682554676));
#29046=CARTESIAN_POINT('Ctrl Pts',(0.185952226875698,-0.156251740320434,
0.266807047398788));
#29047=CARTESIAN_POINT('Ctrl Pts',(-0.030494276369136,-0.240962440043193,
0.255690087090504));
#29048=CARTESIAN_POINT('Ctrl Pts',(-0.18432786741861,-0.130018191841,0.246618580642165));
#29049=CARTESIAN_POINT('Ctrl Pts',(-0.205229924998058,-0.0307899101733451,
0.241252727629919));
#29050=CARTESIAN_POINT('Ctrl Pts',(-0.205152667291151,-5.77023530759641E-5,
0.239592528053768));
#29051=CARTESIAN_POINT('Ctrl Pts',(-0.205152667291151,-5.77023530759641E-5,
0.239592528053768));
#29052=CARTESIAN_POINT('Ctrl Pts',(-0.205057481701977,0.0378060063320381,
0.237547074193825));
#29053=CARTESIAN_POINT('Ctrl Pts',(-0.17685871883546,0.144397474870061,
0.231795966897788));
#29054=CARTESIAN_POINT('Ctrl Pts',(-0.0270112794014323,0.230407377050097,
0.223532257282847));
#29055=CARTESIAN_POINT('Ctrl Pts',(0.088056706918825,0.190765241376624,
0.21731400152785));
#29056=CARTESIAN_POINT('Ctrl Pts',(0.125103714720543,0.162782948353147,
0.214801399208946));
#29057=CARTESIAN_POINT('',(-0.205474970233635,0.00011060057405079,0.245407471946232));
#29058=CARTESIAN_POINT('Ctrl Pts',(-0.205474970233635,0.00011060057405079,
0.245407471946232));
#29059=CARTESIAN_POINT('Ctrl Pts',(-0.205471529321227,0.00650316571769436,
0.245059166525502));
#29060=CARTESIAN_POINT('Ctrl Pts',(-0.205169794342766,0.0128875158726893,
0.244710861104771));
#29061=CARTESIAN_POINT('Ctrl Pts',(-0.204571895687036,0.0192435734730444,
0.244362555684041));
#29062=CARTESIAN_POINT('Ctrl Pts',(-0.203391345348354,0.0317936032830672,
0.243674826955321));
#29063=CARTESIAN_POINT('Ctrl Pts',(-0.201047484118304,0.0442784848425534,
0.242987098226601));
#29064=CARTESIAN_POINT('Ctrl Pts',(-0.197563758380479,0.0564671320289918,
0.242299369497881));
#29065=CARTESIAN_POINT('Ctrl Pts',(-0.194087279374658,0.0686304247913778,
0.241613071359903));
#29066=CARTESIAN_POINT('Ctrl Pts',(-0.189475806558603,0.0804978629125803,
0.240926773221925));
#29067=CARTESIAN_POINT('Ctrl Pts',(-0.183803729986763,0.0918485953510078,
0.240240475083948));
#29068=CARTESIAN_POINT('Ctrl Pts',(-0.178132485468645,0.103197662716856,
0.239554277621077));
#29069=CARTESIAN_POINT('Ctrl Pts',(-0.171401289818514,0.114029381398208,
0.238868080158207));
#29070=CARTESIAN_POINT('Ctrl Pts',(-0.16373207813732,0.124144199275821,
0.238181882695337));
#29071=CARTESIAN_POINT('Ctrl Pts',(-0.156063551213915,0.134258114035796,
0.237495746500701));
#29072=CARTESIAN_POINT('Ctrl Pts',(-0.147457716636604,0.143654580501278,
0.236809610306065));
#29073=CARTESIAN_POINT('Ctrl Pts',(-0.138077400088184,0.152166380024918,
0.236123474111429));
#29074=CARTESIAN_POINT('Ctrl Pts',(-0.128675388147814,0.160697866179164,
0.235435750977419));
#29075=CARTESIAN_POINT('Ctrl Pts',(-0.118495998745998,0.168340063270647,
0.234748027843409));
#29076=CARTESIAN_POINT('Ctrl Pts',(-0.107735027333294,0.17496610960553,
0.234060304709399));
#29077=CARTESIAN_POINT('Ctrl Pts',(-0.103485708862233,0.177582618840717,
0.233788734931519));
#29078=CARTESIAN_POINT('Ctrl Pts',(-0.0991459938811956,0.180041173774481,
0.233517165153638));
#29079=CARTESIAN_POINT('Ctrl Pts',(-0.094728912604613,0.182335977639487,
0.233245595375758));
#29080=CARTESIAN_POINT('Ctrl Pts',(-0.0835430244141027,0.188147376127716,
0.232557867670271));
#29081=CARTESIAN_POINT('Ctrl Pts',(-0.0717812449575055,0.192945918580908,
0.231870139964785));
#29082=CARTESIAN_POINT('Ctrl Pts',(-0.0596504680101255,0.196626034113423,
0.231182412259298));
#29083=CARTESIAN_POINT('Ctrl Pts',(-0.047544925318993,0.200298494326022,
0.230496115154442));
#29084=CARTESIAN_POINT('Ctrl Pts',(-0.035072706489126,0.202856826392769,
0.229809818049586));
#29085=CARTESIAN_POINT('Ctrl Pts',(-0.0224597215775749,0.204243816385363,
0.22912352094473));
#29086=CARTESIAN_POINT('Ctrl Pts',(-0.00984858687894811,0.205630602918836,
0.228437324513567));
#29087=CARTESIAN_POINT('Ctrl Pts',(0.00290241978708712,0.205846247203182,
0.227751128082404));
#29088=CARTESIAN_POINT('Ctrl Pts',(0.0155595115836494,0.204885034163743,
0.227064931651241));
#29089=CARTESIAN_POINT('Ctrl Pts',(0.0282154732632697,0.203923906948376,
0.226378796488672));
#29090=CARTESIAN_POINT('Ctrl Pts',(0.0407766759930771,0.201786220869319,
0.225692661326102));
#29091=CARTESIAN_POINT('Ctrl Pts',(0.0530143360710842,0.198518149789741,
0.225006526163533));
#29092=CARTESIAN_POINT('Ctrl Pts',(0.0652803005675619,0.195242520006062,
0.22431880404262));
#29093=CARTESIAN_POINT('Ctrl Pts',(0.0772204080400473,0.190831566379232,
0.223631081921707));
#29094=CARTESIAN_POINT('Ctrl Pts',(0.0886219140799566,0.185381045335829,
0.222943359800793));
#29095=CARTESIAN_POINT('Ctrl Pts',(0.0931242601512917,0.183228686522827,
0.222671784889687));
#29096=CARTESIAN_POINT('Ctrl Pts',(0.0975428768938958,0.180914732552036,
0.222400209978581));
#29097=CARTESIAN_POINT('Ctrl Pts',(0.101865828789877,0.178446990868301,
0.222128635067475));
#29098=CARTESIAN_POINT('Ctrl Pts',(0.109968665011166,0.173821515688171,
0.221619601638593));
#29099=CARTESIAN_POINT('Ctrl Pts',(0.117776750206857,0.168631069100439,
0.221110568209711));
#29100=CARTESIAN_POINT('Ctrl Pts',(0.125207372047944,0.16292050088877,0.220601534780829));
#29101=CARTESIAN_POINT('Ctrl Pts',(0.125296449978256,0.163038483752231,
0.290616425505885));
#29102=CARTESIAN_POINT('Ctrl Pts',(0.134047410568505,0.156444912057247,
0.290021082642981));
#29103=CARTESIAN_POINT('Ctrl Pts',(0.193248710015229,0.103737668777768,
0.285720086343982));
#29104=CARTESIAN_POINT('Ctrl Pts',(0.235817802334529,-0.0581630255277868,
0.277713436608889));
#29105=CARTESIAN_POINT('Ctrl Pts',(0.078963123396891,-0.229690015875461,
0.266596476300606));
#29106=CARTESIAN_POINT('Ctrl Pts',(-0.143023970547039,-0.192086430267149,
0.255827853965015));
#29107=CARTESIAN_POINT('Ctrl Pts',(-0.205335749874147,-0.0615880815422457,
0.248764885065516));
#29108=CARTESIAN_POINT('Ctrl Pts',(-0.205737936806428,0.000108947515189247,
0.245407569602111));
#29109=CARTESIAN_POINT('Origin',(0.,0.,0.554592528053768));
#29110=CARTESIAN_POINT('',(0.125005569899291,0.162656434463559,0.360610754417505));
#29111=CARTESIAN_POINT('',(0.125373879670659,0.163134317426071,0.354786983357521));
#29112=CARTESIAN_POINT('',(0.125207372047944,0.16292050088877,0.554592528053768));
#29113=CARTESIAN_POINT('',(-0.205269929560708,-0.000254221530507089,0.385407471946233));
#29114=CARTESIAN_POINT('Ctrl Pts',(-0.205269929560708,-0.000254221530507089,
0.385407471946233));
#29115=CARTESIAN_POINT('Ctrl Pts',(-0.204911815068299,0.046813956992531,
0.382860341091967));
#29116=CARTESIAN_POINT('Ctrl Pts',(-0.165590599079174,0.163076528415273,
0.376607556801606));
#29117=CARTESIAN_POINT('Ctrl Pts',(-0.0053899581889141,0.227970089641994,
0.36834198429203));
#29118=CARTESIAN_POINT('Ctrl Pts',(0.0954129300657175,0.185281260987852,
0.36262354263672));
#29119=CARTESIAN_POINT('Ctrl Pts',(0.125005569899291,0.162656434463559,
0.360610754417505));
#29120=CARTESIAN_POINT('',(-0.053017021718863,-0.198517432567172,0.4));
#29121=CARTESIAN_POINT('Ctrl Pts',(-0.0530170217188623,-0.198517432567172,
0.4));
#29122=CARTESIAN_POINT('Ctrl Pts',(-0.11904762702766,-0.180882981070921,
0.396294346563906));
#29123=CARTESIAN_POINT('Ctrl Pts',(-0.192514897068364,-0.111293028538514,
0.391430170545983));
#29124=CARTESIAN_POINT('Ctrl Pts',(-0.205432812329624,-0.0216624454594562,
0.386565994528061));
#29125=CARTESIAN_POINT('Ctrl Pts',(-0.205269929560708,-0.000254221530507089,
0.385407471946233));
#29126=CARTESIAN_POINT('',(0.0530272806035336,-0.198514692496032,0.399999999884365));
#29127=CARTESIAN_POINT('Origin',(0.,0.,0.4));
#29128=CARTESIAN_POINT('',(-0.205474945991894,0.00014897861661356,0.379592528053768));
#29129=CARTESIAN_POINT('Ctrl Pts',(0.0530272806035336,-0.198514692496032,
0.399999999884365));
#29130=CARTESIAN_POINT('Ctrl Pts',(0.0408717438820405,-0.201761681666015,
0.39931360375684));
#29131=CARTESIAN_POINT('Ctrl Pts',(0.0283736580848827,-0.20389956149503,
0.398627207629315));
#29132=CARTESIAN_POINT('Ctrl Pts',(0.0157570658297097,-0.204869935572397,
0.39794081150179));
#29133=CARTESIAN_POINT('Ctrl Pts',(0.00316664435563644,-0.205838296788681,
0.397255839175751));
#29134=CARTESIAN_POINT('Ctrl Pts',(-0.00954094414690598,-0.205643818959396,
0.396570866849711));
#29135=CARTESIAN_POINT('Ctrl Pts',(-0.0221335092146457,-0.204279424795659,
0.395885894523672));
#29136=CARTESIAN_POINT('Ctrl Pts',(-0.0347240236104722,-0.202915252820552,
0.395201033743891));
#29137=CARTESIAN_POINT('Ctrl Pts',(-0.0471986847358641,-0.200381590770703,
0.394516172964109));
#29138=CARTESIAN_POINT('Ctrl Pts',(-0.0593287840410988,-0.196723336209014,
0.393831312184328));
#29139=CARTESIAN_POINT('Ctrl Pts',(-0.0714581310177007,-0.193065308538266,
0.393146493880734));
#29140=CARTESIAN_POINT('Ctrl Pts',(-0.083242134706469,-0.188283102977198,
0.392461675577141));
#29141=CARTESIAN_POINT('Ctrl Pts',(-0.0944682472819012,-0.18247116451781,
0.391776857273547));
#29142=CARTESIAN_POINT('Ctrl Pts',(-0.105719366886094,-0.176646279518715,
0.391090513484537));
#29143=CARTESIAN_POINT('Ctrl Pts',(-0.116409373895057,-0.169787539362461,
0.390404169695527));
#29144=CARTESIAN_POINT('Ctrl Pts',(-0.126352259228902,-0.162034200750188,
0.389717825906517));
#29145=CARTESIAN_POINT('Ctrl Pts',(-0.129366540326112,-0.159683701751704,
0.389509754200978));
#29146=CARTESIAN_POINT('Ctrl Pts',(-0.132312391393676,-0.15725126197307,
0.389301682495438));
#29147=CARTESIAN_POINT('Ctrl Pts',(-0.135185282742093,-0.154741445498419,
0.389093610789898));
#29148=CARTESIAN_POINT('Ctrl Pts',(-0.144554550829065,-0.146556261811243,
0.38841503323367));
#29149=CARTESIAN_POINT('Ctrl Pts',(-0.153213834910319,-0.137485213545017,
0.387736455677443));
#29150=CARTESIAN_POINT('Ctrl Pts',(-0.16099192577821,-0.127677623173457,
0.387057878121216));
#29151=CARTESIAN_POINT('Ctrl Pts',(-0.168758910581936,-0.117884036717488,
0.38638026948217));
#29152=CARTESIAN_POINT('Ctrl Pts',(-0.175646580121297,-0.107356630055652,
0.385702660843124));
#29153=CARTESIAN_POINT('Ctrl Pts',(-0.181521398102516,-0.0962806193161842,
0.385025052204078));
#29154=CARTESIAN_POINT('Ctrl Pts',(-0.187390823725915,-0.0852147749875414,
0.38434806552613));
#29155=CARTESIAN_POINT('Ctrl Pts',(-0.192248809751825,-0.0736021027695189,
0.383671078848182));
#29156=CARTESIAN_POINT('Ctrl Pts',(-0.196007247674439,-0.0616533412240657,
0.382994092170234));
#29157=CARTESIAN_POINT('Ctrl Pts',(-0.199772028850871,-0.0496844133145936,
0.382315962916988));
#29158=CARTESIAN_POINT('Ctrl Pts',(-0.202433306145674,-0.037379121243756,
0.381637833663743));
#29159=CARTESIAN_POINT('Ctrl Pts',(-0.203952980621335,-0.024963119209617,
0.380959704410497));
#29160=CARTESIAN_POINT('Ctrl Pts',(-0.204974252501832,-0.0166191521635482,
0.380503978958254));
#29161=CARTESIAN_POINT('Ctrl Pts',(-0.205481017838544,-0.00822546055280679,
0.380048253506011));
#29162=CARTESIAN_POINT('Ctrl Pts',(-0.205474945991894,0.00014897861661356,
0.379592528053768));
#29163=CARTESIAN_POINT('Ctrl Pts',(-0.205652323534904,0.000149107223343921,
0.379592528053768));
#29164=CARTESIAN_POINT('Ctrl Pts',(-0.20573550917628,0.010055539256624,
0.379053902196384));
#29165=CARTESIAN_POINT('Ctrl Pts',(-0.200581379579465,0.0880330322633288,
0.374809622902905));
#29166=CARTESIAN_POINT('Ctrl Pts',(-0.100785874709386,0.221009791285371,
0.366859690173332));
#29167=CARTESIAN_POINT('Ctrl Pts',(0.060421068680088,0.209514631200961,
0.359129801131968));
#29168=CARTESIAN_POINT('Ctrl Pts',(0.120756096920903,0.166732102669948,
0.355105565526697));
#29169=CARTESIAN_POINT('Ctrl Pts',(0.125373879670659,0.163134317426071,
0.354786983357521));
#29170=CARTESIAN_POINT('Origin',(0.,0.,0.2));
#29171=CARTESIAN_POINT('',(-0.156342830367367,0.0575541431412261,0.00322368732047967));
#29172=CARTESIAN_POINT('',(-0.156342830367367,0.0575541431412265,0.));
#29173=CARTESIAN_POINT('',(-0.156342830367367,0.0575541431412265,0.2));
#29174=CARTESIAN_POINT('',(-0.133525467299036,0.0997593943732614,4.94193308168658E-8));
#29175=CARTESIAN_POINT('Origin',(0.,0.,0.));
#29176=CARTESIAN_POINT('Ctrl Pts',(-0.133464457974224,0.0997135821122009,
4.94960437080749E-8));
#29177=CARTESIAN_POINT('Ctrl Pts',(-0.139892380533608,0.0911099477615352,
0.000722668837111375));
#29178=CARTESIAN_POINT('Ctrl Pts',(-0.145510047094401,0.0818485169225855,
0.00144528817817908));
#29179=CARTESIAN_POINT('Ctrl Pts',(-0.150187465421622,0.072106069302308,
0.00216790751924678));
#29180=CARTESIAN_POINT('Ctrl Pts',(-0.152465439227535,0.0673613492597746,
0.00251983411965774));
#29181=CARTESIAN_POINT('Ctrl Pts',(-0.154520997855119,0.0625030562146302,
0.00287176072006871));
#29182=CARTESIAN_POINT('Ctrl Pts',(-0.156342830367367,0.0575541431412261,
0.00322368732047967));
#29183=CARTESIAN_POINT('Origin',(0.,0.,0.2));
#29184=CARTESIAN_POINT('',(-0.156342830139253,0.0575541437608846,0.0733422317177101));
#29185=CARTESIAN_POINT('',(-0.156342830367367,0.0575541431412264,0.0539160112414913));
#29186=CARTESIAN_POINT('',(-0.156342830367367,0.0575541431412265,0.2));
#29187=CARTESIAN_POINT('',(-0.0769902040670466,-0.147743251885541,0.));
#29188=CARTESIAN_POINT('Ctrl Pts',(-0.156342830367367,0.0575541431412264,
0.0539160112414913));
#29189=CARTESIAN_POINT('Ctrl Pts',(-0.152615756398934,0.0676785453373198,
0.0531935750919307));
#29190=CARTESIAN_POINT('Ctrl Pts',(-0.147891507930115,0.0774656277419028,
0.05247113894237));
#29191=CARTESIAN_POINT('Ctrl Pts',(-0.142255363256947,0.0867120039246811,
0.0517487027928093));
#29192=CARTESIAN_POINT('Ctrl Pts',(-0.136621244092119,0.0959550571600989,
0.0510265262711557));
#29193=CARTESIAN_POINT('Ctrl Pts',(-0.130076306162921,0.104656981987856,
0.050304349749502));
#29194=CARTESIAN_POINT('Ctrl Pts',(-0.122751565884437,0.112639305186594,
0.0495821732278483));
#29195=CARTESIAN_POINT('Ctrl Pts',(-0.11542826033528,0.120620064852326,
0.048860138162109));
#29196=CARTESIAN_POINT('Ctrl Pts',(-0.107326090505026,0.127880844210078,
0.0481381030963697));
#29197=CARTESIAN_POINT('Ctrl Pts',(-0.0986138651527419,0.134279058678697,
0.0474160680306305));
#29198=CARTESIAN_POINT('Ctrl Pts',(-0.0898809033414771,0.140692501898468,
0.0466923144085044));
#29199=CARTESIAN_POINT('Ctrl Pts',(-0.0805357626312733,0.146238792804792,
0.0459685607863782));
#29200=CARTESIAN_POINT('Ctrl Pts',(-0.0707758351420504,0.150818901865599,
0.0452448071642521));
#29201=CARTESIAN_POINT('Ctrl Pts',(-0.0672833339567882,0.152457852189888,
0.0449858185205451));
#29202=CARTESIAN_POINT('Ctrl Pts',(-0.0637379152078948,0.153973529339594,
0.044726829876838));
#29203=CARTESIAN_POINT('Ctrl Pts',(-0.0601491615363001,0.155362924684366,
0.044467841233131));
#29204=CARTESIAN_POINT('Ctrl Pts',(-0.0500871093811335,0.159258474421843,
0.0437416957578361));
#29205=CARTESIAN_POINT('Ctrl Pts',(-0.0396085706270415,0.162186610709678,
0.0430155502825413));
#29206=CARTESIAN_POINT('Ctrl Pts',(-0.0289208966445087,0.164070538907135,
0.0422894048072465));
#29207=CARTESIAN_POINT('Ctrl Pts',(-0.0179575253928811,0.166003064569302,
0.0415445278170466));
#29208=CARTESIAN_POINT('Ctrl Pts',(-0.00677497403134137,0.166836279722674,
0.0407996508268468));
#29209=CARTESIAN_POINT('Ctrl Pts',(0.00438737489389764,0.16654221969681,
0.040054773836647));
#29210=CARTESIAN_POINT('Ctrl Pts',(0.015243375983249,0.166256230073792,
0.0393303398065695));
#29211=CARTESIAN_POINT('Ctrl Pts',(0.0260793197013875,0.164904216308862,
0.038605905776492));
#29212=CARTESIAN_POINT('Ctrl Pts',(0.0366743509548406,0.162513236328741,
0.0378814717464145));
#29213=CARTESIAN_POINT('Ctrl Pts',(0.0477178574160074,0.160021048979093,
0.0371263732761536));
#29214=CARTESIAN_POINT('Ctrl Pts',(0.0584985092249134,0.156399957609841,
0.0363712748058926));
#29215=CARTESIAN_POINT('Ctrl Pts',(0.0687813422296158,0.151738877553159,
0.0356161763356316));
#29216=CARTESIAN_POINT('Ctrl Pts',(0.0790641752343186,0.147077797496476,
0.0348610778653706));
#29217=CARTESIAN_POINT('Ctrl Pts',(0.0888482470888435,0.141377313875567,
0.0341059793951096));
#29218=CARTESIAN_POINT('Ctrl Pts',(0.0979290929616005,0.134779274191985,
0.0333508809248486));
#29219=CARTESIAN_POINT('Ctrl Pts',(0.106657202728024,0.128437528565149,
0.0326251134770529));
#29220=CARTESIAN_POINT('Ctrl Pts',(0.114797950788352,0.121221776032182,
0.0318993460292573));
#29221=CARTESIAN_POINT('Ctrl Pts',(0.122174628985777,0.113264822571652,
0.0311735785814616));
#29222=CARTESIAN_POINT('Ctrl Pts',(0.12974649655419,0.105097325462697,0.0304286070843869));
#29223=CARTESIAN_POINT('Ctrl Pts',(0.136512390637496,0.0961493361664923,
0.0296836355873123));
#29224=CARTESIAN_POINT('Ctrl Pts',(0.142319108061956,0.0866073408000109,
0.0289386640902376));
#29225=CARTESIAN_POINT('Ctrl Pts',(0.147963582781976,0.077331953746084,
0.0282145074841902));
#29226=CARTESIAN_POINT('Ctrl Pts',(0.152701412631395,0.0674962147486724,
0.0274903508781428));
#29227=CARTESIAN_POINT('Ctrl Pts',(0.156435984337242,0.0573004607698592,
0.0267661942720954));
#29228=CARTESIAN_POINT('Ctrl Pts',(0.160331573775527,0.0466651122898616,
0.0260108153295071));
#29229=CARTESIAN_POINT('Ctrl Pts',(0.163134817554856,0.0356389106652969,
0.0252554363869188));
#29230=CARTESIAN_POINT('Ctrl Pts',(0.164793439816337,0.0244679830288367,
0.0245000574443305));
#29231=CARTESIAN_POINT('Ctrl Pts',(0.166452062077817,0.0132970553923761,
0.0237446785017422));
#29232=CARTESIAN_POINT('Ctrl Pts',(0.166966048451613,0.0019825153896915,
0.0229892995591539));
#29233=CARTESIAN_POINT('Ctrl Pts',(0.166344308986419,-0.00922663903221849,
0.0222339206165656));
#29234=CARTESIAN_POINT('Ctrl Pts',(0.165754249536044,-0.0198646439645363,
0.0215170311336875));
#29235=CARTESIAN_POINT('Ctrl Pts',(0.164136945659952,-0.0304899505688286,
0.0208001416508095));
#29236=CARTESIAN_POINT('Ctrl Pts',(0.161504983847412,-0.0408864304194841,
0.0200832521679314));
#29237=CARTESIAN_POINT('Ctrl Pts',(0.158761774196747,-0.051722348981587,
0.0193360611796274));
#29238=CARTESIAN_POINT('Ctrl Pts',(0.154916029353243,-0.06230855393879,
0.0185888701913233));
#29239=CARTESIAN_POINT('Ctrl Pts',(0.150041776687632,-0.0724087373762231,
0.0178416792030193));
#29240=CARTESIAN_POINT('Ctrl Pts',(0.145375225859147,-0.0820785314187703,
0.017126327545091));
#29241=CARTESIAN_POINT('Ctrl Pts',(0.139766704504901,-0.0913020834547842,
0.0164109758871627));
#29242=CARTESIAN_POINT('Ctrl Pts',(0.133329944446156,-0.0998933727230443,
0.0156956242292345));
#29243=CARTESIAN_POINT('Ctrl Pts',(0.12689205686693,-0.108486166918397,
0.0149801472639098));
#29244=CARTESIAN_POINT('Ctrl Pts',(0.119626238227325,-0.116445760369784,
0.014264670298585));
#29245=CARTESIAN_POINT('Ctrl Pts',(0.111686655558303,-0.123618974960161,
0.0135491933332603));
#29246=CARTESIAN_POINT('Ctrl Pts',(0.103726328226589,-0.130810931835026,
0.012831846958808));
#29247=CARTESIAN_POINT('Ctrl Pts',(0.0950894792843525,-0.137211862084236,
0.0121145005843559));
#29248=CARTESIAN_POINT('Ctrl Pts',(0.0859617718008449,-0.142709963873794,
0.0113971542099036));
#29249=CARTESIAN_POINT('Ctrl Pts',(0.0847733510398566,-0.143425812658885,
0.0113037562426968));
#29250=CARTESIAN_POINT('Ctrl Pts',(0.0835766414215304,-0.14412642177342,
0.0112103582754899));
#29251=CARTESIAN_POINT('Ctrl Pts',(0.0823720791733835,-0.144811603722401,
0.011116960308283));
#29252=CARTESIAN_POINT('Ctrl Pts',(0.0727647703535419,-0.150276455864141,
0.0103720398066797));
#29253=CARTESIAN_POINT('Ctrl Pts',(0.0625826554862529,-0.154797868787369,
0.0096271193050763));
#29254=CARTESIAN_POINT('Ctrl Pts',(0.0520293316166242,-0.158267206494357,
0.00888219880347299));
#29255=CARTESIAN_POINT('Ctrl Pts',(0.0415003014352618,-0.161728557806747,
0.00813899310439756));
#29256=CARTESIAN_POINT('Ctrl Pts',(0.0306025347797131,-0.164142306937139,
0.0073957874053221));
#29257=CARTESIAN_POINT('Ctrl Pts',(0.019559542774564,-0.165447829500571,
0.00665258170624666));
#29258=CARTESIAN_POINT('Ctrl Pts',(0.00853395449654739,-0.166751294563785,
0.00591054729745052));
#29259=CARTESIAN_POINT('Ctrl Pts',(-0.00263556846420341,-0.166949863901546,
0.00516851288865437));
#29260=CARTESIAN_POINT('Ctrl Pts',(-0.0137173127653849,-0.166034319736904,
0.00442647847985822));
#29261=CARTESIAN_POINT('Ctrl Pts',(-0.0248064277508162,-0.165118166625984,
0.0036839505295057));
#29262=CARTESIAN_POINT('Ctrl Pts',(-0.0358067961519084,-0.163086461087822,
0.00294142257915325));
#29263=CARTESIAN_POINT('Ctrl Pts',(-0.0464896508237926,-0.159982100143366,
0.00219889462880074));
#29264=CARTESIAN_POINT('Ctrl Pts',(-0.0570349201958577,-0.1569177205002,
0.00146592975253386));
#29265=CARTESIAN_POINT('Ctrl Pts',(-0.0672700612540289,-0.152808496958899,
0.000732964876266929));
#29266=CARTESIAN_POINT('Ctrl Pts',(-0.0769902040670455,-0.147743251885542,
5.55111512312578E-17));
#29267=CARTESIAN_POINT('Origin',(0.,0.,0.));
#29268=CARTESIAN_POINT('',(-0.166599954470727,-0.000123167981316404,0.00714803633902117));
#29269=CARTESIAN_POINT('Ctrl Pts',(-0.156342830367367,0.0575541431412261,
0.00322368732047967));
#29270=CARTESIAN_POINT('Ctrl Pts',(-0.160075959044492,0.0474132936445152,
0.00394482237290883));
#29271=CARTESIAN_POINT('Ctrl Pts',(-0.16282449732221,0.0368910332598892,
0.004665957425338));
#29272=CARTESIAN_POINT('Ctrl Pts',(-0.164527021450747,0.0261996032898461,
0.00538709247776717));
#29273=CARTESIAN_POINT('Ctrl Pts',(-0.165912822627511,0.0174971150340725,
0.00597407376485183));
#29274=CARTESIAN_POINT('Ctrl Pts',(-0.166606465027433,0.00868316658102717,
0.00656105505193651));
#29275=CARTESIAN_POINT('Ctrl Pts',(-0.166599954470727,-0.000123167981316404,
0.00714803633902117));
#29276=CARTESIAN_POINT('Ctrl Pts',(-0.166599958397467,-0.000117736835231835,
0.00723493944780304));
#29277=CARTESIAN_POINT('Ctrl Pts',(-0.166592368206091,-0.0108580082624692,
0.00790617652409698));
#29278=CARTESIAN_POINT('Ctrl Pts',(-0.165546235023722,-0.0215724161967638,
0.00855403105481129));
#29279=CARTESIAN_POINT('Ctrl Pts',(-0.162441244087431,-0.0373794110721927,
0.00955409310228141));
#29280=CARTESIAN_POINT('Ctrl Pts',(-0.161152620668966,-0.0425934270508658,
0.00989185324071785));
#29281=CARTESIAN_POINT('Ctrl Pts',(-0.159055055717249,-0.0496071060965288,
0.0103680472660056));
#29282=CARTESIAN_POINT('Ctrl Pts',(-0.158462514085925,-0.0514685001513247,
0.0104965848910276));
#29283=CARTESIAN_POINT('Ctrl Pts',(-0.157350802925274,-0.0547594435620609,
0.0107284149417728));
#29284=CARTESIAN_POINT('Ctrl Pts',(-0.156844552891193,-0.0561930377736858,
0.0108310190040426));
#29285=CARTESIAN_POINT('Ctrl Pts',(-0.155543472955219,-0.0597228008901498,
0.0110876343866849));
#29286=CARTESIAN_POINT('Ctrl Pts',(-0.154725867189838,-0.0618101100221925,
0.0112428263475635));
#29287=CARTESIAN_POINT('Ctrl Pts',(-0.150165835048625,-0.0727937397929403,
0.0120755817193222));
#29288=CARTESIAN_POINT('Ctrl Pts',(-0.145697941630321,-0.0813682410202298,
0.0127813383790904));
#29289=CARTESIAN_POINT('Ctrl Pts',(-0.135157226586141,-0.0979156585876231,
0.0142067535748699));
#29290=CARTESIAN_POINT('Ctrl Pts',(-0.129056335196386,-0.105827549577747,
0.0149229165520539));
#29291=CARTESIAN_POINT('Ctrl Pts',(-0.120037218891217,-0.115574936681505,
0.0158413941168924));
#29292=CARTESIAN_POINT('Ctrl Pts',(-0.117718951883375,-0.117935367779911,
0.0160672245974781));
#29293=CARTESIAN_POINT('Ctrl Pts',(-0.113458916973888,-0.122022005173732,
0.0164648200388858));
#29294=CARTESIAN_POINT('Ctrl Pts',(-0.111544231225263,-0.123774720228262,
0.0166377011249371));
#29295=CARTESIAN_POINT('Ctrl Pts',(-0.10725320154447,-0.127522274301523,
0.0170131168076669));
#29296=CARTESIAN_POINT('Ctrl Pts',(-0.104860493546977,-0.129496944483681,
0.0172147810714845));
#29297=CARTESIAN_POINT('Ctrl Pts',(-0.0973081156948805,-0.135383142208357,
0.017829906463473));
#29298=CARTESIAN_POINT('Ctrl Pts',(-0.0919744243385157,-0.139061794399417,
0.0182345513585974));
#29299=CARTESIAN_POINT('Ctrl Pts',(-0.0779129673261363,-0.147596126968494,
0.0192487804156516));
#29300=CARTESIAN_POINT('Ctrl Pts',(-0.0689391260660634,-0.151994836564664,
0.0198481246745527));
#29301=CARTESIAN_POINT('Ctrl Pts',(-0.0551441590205115,-0.157282297394672,
0.0207662746777883));
#29302=CARTESIAN_POINT('Ctrl Pts',(-0.0505904342340529,-0.15880553729486,
0.0210691251433191));
#29303=CARTESIAN_POINT('Ctrl Pts',(-0.0441746294974275,-0.160647693709756,
0.0215035785467938));
#29304=CARTESIAN_POINT('Ctrl Pts',(-0.0423629661008501,-0.161134905313752,
0.0216271032871064));
#29305=CARTESIAN_POINT('Ctrl Pts',(-0.0391022697005884,-0.161953019748277,
0.0218515749498044));
#29306=CARTESIAN_POINT('Ctrl Pts',(-0.0376563782906403,-0.162295300820419,
0.0219519065039507));
#29307=CARTESIAN_POINT('Ctrl Pts',(-0.0344156680042966,-0.163016828708008,
0.0221784773177518));
#29308=CARTESIAN_POINT('Ctrl Pts',(-0.0326188426827027,-0.16338584711307,
0.0223052104047674));
#29309=CARTESIAN_POINT('Ctrl Pts',(-0.0245482288464476,-0.164904900506212,
0.0228783100832908));
#29310=CARTESIAN_POINT('Ctrl Pts',(-0.0182180557007977,-0.165723651928309,
0.02333803504725));
#29311=CARTESIAN_POINT('Ctrl Pts',(-0.00266982004660984,-0.166833060022998,
0.024470488153681));
#29312=CARTESIAN_POINT('Ctrl Pts',(0.00655685279637343,-0.166725607649479,
0.0251444914691373));
#29313=CARTESIAN_POINT('Ctrl Pts',(0.0214036166788052,-0.165317727473419,
0.02620817517656));
#29314=CARTESIAN_POINT('Ctrl Pts',(0.027048668748578,-0.164488443891499,
0.0266079380167437));
#29315=CARTESIAN_POINT('Ctrl Pts',(0.0354882404179006,-0.162802264009165,
0.0271978686362366));
#29316=CARTESIAN_POINT('Ctrl Pts',(0.0383206014720584,-0.162158952090207,
0.027394550835668));
#29317=CARTESIAN_POINT('Ctrl Pts',(0.0436379708253891,-0.160804103888315,
0.0277616805416717));
#29318=CARTESIAN_POINT('Ctrl Pts',(0.0461260205228799,-0.160108162928327,
0.0279325756683645));
#29319=CARTESIAN_POINT('Ctrl Pts',(0.0519592080958445,-0.158329265883714,
0.0283316986612704));
#29320=CARTESIAN_POINT('Ctrl Pts',(0.0552882965295458,-0.157197719114055,
0.0285582573366589));
#29321=CARTESIAN_POINT('Ctrl Pts',(0.0682544247256167,-0.152327631974431,
0.0294393615905225));
#29322=CARTESIAN_POINT('Ctrl Pts',(0.0775706675717061,-0.147801187405166,
0.0300679352278671));
#29323=CARTESIAN_POINT('Ctrl Pts',(0.0917563256834444,-0.13919578656551,
0.0310798904630806));
#29324=CARTESIAN_POINT('Ctrl Pts',(0.0969173310599853,-0.135652910945856,
0.0314617418059934));
#29325=CARTESIAN_POINT('Ctrl Pts',(0.104003512100219,-0.130177273155847,
0.0320234510840598));
#29326=CARTESIAN_POINT('Ctrl Pts',(0.106099843565373,-0.128474412091306,
0.0321947291697927));
#29327=CARTESIAN_POINT('Ctrl Pts',(0.109817288218199,-0.125301661601329,
0.03250977571567));
#29328=CARTESIAN_POINT('Ctrl Pts',(0.111452611561631,-0.123849333474221,
0.0326525543144872));
#29329=CARTESIAN_POINT('Ctrl Pts',(0.114148068623023,-0.121358880726997,
0.0328959944787813));
#29330=CARTESIAN_POINT('Ctrl Pts',(0.115223743450111,-0.120338057850148,
0.0329954332102852));
#29331=CARTESIAN_POINT('Ctrl Pts',(0.117628426211631,-0.117994190888653,
0.0332231479315271));
#29332=CARTESIAN_POINT('Ctrl Pts',(0.118948878478074,-0.116662930084048,
0.0333519923055864));
#29333=CARTESIAN_POINT('Ctrl Pts',(0.123212799975926,-0.112216457135386,
0.0337798979674513));
#29334=CARTESIAN_POINT('Ctrl Pts',(0.126058385322084,-0.109010112184116,
0.0340846098461402));
#29335=CARTESIAN_POINT('Ctrl Pts',(0.135780660084974,-0.0971649913331188,
0.0351869742860296));
#29336=CARTESIAN_POINT('Ctrl Pts',(0.141919086720901,-0.087956919649469,
0.0359998247712268));
#29337=CARTESIAN_POINT('Ctrl Pts',(0.150003673060108,-0.0727507328644793,
0.0372322330029602));
#29338=CARTESIAN_POINT('Ctrl Pts',(0.152599775061937,-0.0671349060529186,
0.0376670365958292));
#29339=CARTESIAN_POINT('Ctrl Pts',(0.155977327425111,-0.0586134399364334,
0.0382963863519817));
#29340=CARTESIAN_POINT('Ctrl Pts',(0.157002052364009,-0.0558105686102229,
0.0384987729075076));
#29341=CARTESIAN_POINT('Ctrl Pts',(0.158777867577763,-0.0505164247947176,
0.0388728636293751));
#29342=CARTESIAN_POINT('Ctrl Pts',(0.159546950652165,-0.0480322000286018,
0.0390451156607787));
#29343=CARTESIAN_POINT('Ctrl Pts',(0.161187407552089,-0.042258189614945,
0.0394385112086754));
#29344=CARTESIAN_POINT('Ctrl Pts',(0.162016790525698,-0.0389576326242932,
0.0396582455843352));
#29345=CARTESIAN_POINT('Ctrl Pts',(0.164360440706438,-0.0282538518820897,
0.0403570546296552));
#29346=CARTESIAN_POINT('Ctrl Pts',(0.165472557282312,-0.0207721785598963,
0.0408241048564408));
#29347=CARTESIAN_POINT('Ctrl Pts',(0.166729528251484,-0.00500592924388155,
0.0417931774538173));
#29348=CARTESIAN_POINT('Ctrl Pts',(0.166772658709673,0.00326539906077528,
0.0422930461371366));
#29349=CARTESIAN_POINT('Ctrl Pts',(0.16589872011113,0.0158899850704833,
0.0430826823877555));
#29350=CARTESIAN_POINT('Ctrl Pts',(0.165421832421319,0.020260489237606,
0.0433611254795038));
#29351=CARTESIAN_POINT('Ctrl Pts',(0.164502508173179,0.0264165420258095,
0.0437669086990131));
#29352=CARTESIAN_POINT('Ctrl Pts',(0.16420243155374,0.0282217935483682,
0.0438875793531755));
#29353=CARTESIAN_POINT('Ctrl Pts',(0.163601369373112,0.0315026833445796,
0.0441105555291625));
#29354=CARTESIAN_POINT('Ctrl Pts',(0.163310006948505,0.0329798126116908,
0.0442123581354838));
#29355=CARTESIAN_POINT('Ctrl Pts',(0.162520207385939,0.0367164188842215,
0.044473306171508));
#29356=CARTESIAN_POINT('Ctrl Pts',(0.161994660715965,0.0389697544497462,
0.044633816515132));
#29357=CARTESIAN_POINT('Ctrl Pts',(0.159542247628278,0.0485757295139883,
0.0453295725218254));
#29358=CARTESIAN_POINT('Ctrl Pts',(0.157160471842514,0.055802309349271,
0.0458816939421));
#29359=CARTESIAN_POINT('Ctrl Pts',(0.15128179773945,0.070236397576997,0.0470160618690842));
#29360=CARTESIAN_POINT('Ctrl Pts',(0.147741471496556,0.0774067841388483,
0.0475968391062373));
#29361=CARTESIAN_POINT('Ctrl Pts',(0.141010981183482,0.0888803208855026,
0.048542005694306));
#29362=CARTESIAN_POINT('Ctrl Pts',(0.138103698186968,0.0933337413707272,
0.04891343187207));
#29363=CARTESIAN_POINT('Ctrl Pts',(0.133309512225687,0.0999616803598096,
0.0494731580193658));
#29364=CARTESIAN_POINT('Ctrl Pts',(0.131571215043564,0.102238841634508,
0.0496668486853999));
#29365=CARTESIAN_POINT('Ctrl Pts',(0.128130948366677,0.106512410466517,
0.0500334252771629));
#29366=CARTESIAN_POINT('Ctrl Pts',(0.126438878506964,0.108515643282706,
0.0502066325359914));
#29367=CARTESIAN_POINT('Ctrl Pts',(0.122638968076052,0.112804719032673,
0.050581118478324));
#29368=CARTESIAN_POINT('Ctrl Pts',(0.12051298923741,0.115073205116196,0.0507815652600641));
#29369=CARTESIAN_POINT('Ctrl Pts',(0.109219872710163,0.126466817527054,
0.0518041790836088));
#29370=CARTESIAN_POINT('Ctrl Pts',(0.099076625939989,0.134561062337971,
0.0525811797134423));
#29371=CARTESIAN_POINT('Ctrl Pts',(0.0822802446722472,0.145025918412974,
0.0537957833936754));
#29372=CARTESIAN_POINT('Ctrl Pts',(0.0762442217714142,0.148288076622371,
0.0542210374384404));
#29373=CARTESIAN_POINT('Ctrl Pts',(0.0681818604012453,0.152022764751916,
0.0547965324269851));
#29374=CARTESIAN_POINT('Ctrl Pts',(0.0663231457275668,0.15284281623537,
0.0549297129416109));
#29375=CARTESIAN_POINT('Ctrl Pts',(0.0632178415163958,0.154145547979268,
0.055153797117645));
#29376=CARTESIAN_POINT('Ctrl Pts',(0.0619796373186184,0.15464756626802,
0.0552435823339178));
#29377=CARTESIAN_POINT('Ctrl Pts',(0.0589549166825762,0.155831749423144,
0.055464056201819));
#29378=CARTESIAN_POINT('Ctrl Pts',(0.0571625872232252,0.156498096218549,
0.0555955943497492));
#29379=CARTESIAN_POINT('Ctrl Pts',(0.0508956524107808,0.158705984870631,
0.0560576521350662));
#29380=CARTESIAN_POINT('Ctrl Pts',(0.0463674110114099,0.160087514516793,
0.0563952002162176));
#29381=CARTESIAN_POINT('Ctrl Pts',(0.0315119747698736,0.163936629537465,
0.057502197453484));
#29382=CARTESIAN_POINT('Ctrl Pts',(0.0210051869178905,0.165611078142225,
0.0582827516981497));
#29383=CARTESIAN_POINT('Ctrl Pts',(0.00434482380566355,0.166654190916582,
0.0594765282641642));
#29384=CARTESIAN_POINT('Ctrl Pts',(-0.00173765817253539,0.166701807412088,
0.0599037483930031));
#29385=CARTESIAN_POINT('Ctrl Pts',(-0.0107704108373828,0.166277908332304,
0.0605243993235179));
#29386=CARTESIAN_POINT('Ctrl Pts',(-0.0137269451190884,0.166059981624386,
0.0607253865402798));
#29387=CARTESIAN_POINT('Ctrl Pts',(-0.0192548989393031,0.165503853496326,
0.0610974911352458));
#29388=CARTESIAN_POINT('Ctrl Pts',(-0.0218272444225489,0.165184289034333,
0.0612691384770206));
#29389=CARTESIAN_POINT('Ctrl Pts',(-0.0278163545184306,0.164297897039467,
0.0616658175862565));
#29390=CARTESIAN_POINT('Ctrl Pts',(-0.0312250363416327,0.163684294949153,
0.0618893045697229));
#29391=CARTESIAN_POINT('Ctrl Pts',(-0.0424408363650814,0.161302156188398,
0.0626199091541332));
#29392=CARTESIAN_POINT('Ctrl Pts',(-0.0501397394947855,0.159077448715882,
0.0631131610859068));
#29393=CARTESIAN_POINT('Ctrl Pts',(-0.0651021964221637,0.153558985352872,
0.064088440714332));
#29394=CARTESIAN_POINT('Ctrl Pts',(-0.0723483781403307,0.150280930274018,
0.0645693842021876));
#29395=CARTESIAN_POINT('Ctrl Pts',(-0.0831251800423115,0.144445024272915,
0.0653342910209706));
#29396=CARTESIAN_POINT('Ctrl Pts',(-0.0868361443326735,0.14224499293338,
0.0656076354806959));
#29397=CARTESIAN_POINT('Ctrl Pts',(-0.0919812432414162,0.138918337239207,
0.0660071111989614));
#29398=CARTESIAN_POINT('Ctrl Pts',(-0.093488958250325,0.137908185032123,
0.0661267942824281));
#29399=CARTESIAN_POINT('Ctrl Pts',(-0.0962138620331477,0.136017311492476,
0.066348533201565));
#29400=CARTESIAN_POINT('Ctrl Pts',(-0.097436157328333,0.135144407202752,
0.0664501044180121));
#29401=CARTESIAN_POINT('Ctrl Pts',(-0.10051080020847,0.132885256902538,
0.0667108162502505));
#29402=CARTESIAN_POINT('Ctrl Pts',(-0.102346319394633,0.131476773628673,
0.0668713303880289));
#29403=CARTESIAN_POINT('Ctrl Pts',(-0.110011714962414,0.125336952892199,
0.0675606381958586));
#29404=CARTESIAN_POINT('Ctrl Pts',(-0.115547179363288,0.120252901228537,
0.0681058875832981));
#29405=CARTESIAN_POINT('Ctrl Pts',(-0.126270803986498,0.108977555315009,
0.0692385558110044));
#29406=CARTESIAN_POINT('Ctrl Pts',(-0.13139106418083,0.102746439399671,
0.0698245284256865));
#29407=CARTESIAN_POINT('Ctrl Pts',(-0.139123253083575,0.0918084760142583,
0.0707765744402518));
#29408=CARTESIAN_POINT('Ctrl Pts',(-0.141994577432469,0.0873019267885008,
0.0711498417046757));
#29409=CARTESIAN_POINT('Ctrl Pts',(-0.146067692229229,0.0801748940696286,
0.0717116070706711));
#29410=CARTESIAN_POINT('Ctrl Pts',(-0.147426208465994,0.0776485620823815,
0.0719055645261873));
#29411=CARTESIAN_POINT('Ctrl Pts',(-0.149899905865631,0.0727491877081231,
0.0722723242475758));
#29412=CARTESIAN_POINT('Ctrl Pts',(-0.151025615460698,0.0703824614936514,
0.0724454558319081));
#29413=CARTESIAN_POINT('Ctrl Pts',(-0.153360678588948,0.0651588789322013,
0.0728194286729711));
#29414=CARTESIAN_POINT('Ctrl Pts',(-0.154547038060658,0.0622927944332981,
0.0730194484095675));
#29415=CARTESIAN_POINT('Ctrl Pts',(-0.155886421924921,0.0587827612910115,
0.0732589751331156));
#29416=CARTESIAN_POINT('Ctrl Pts',(-0.156116449063536,0.0581690961475399,
0.0733006546124061));
#29417=CARTESIAN_POINT('Ctrl Pts',(-0.156342830139253,0.0575541437608846,
0.0733422317177101));
#29418=CARTESIAN_POINT('Origin',(0.,0.,0.2));
#29419=CARTESIAN_POINT('',(-0.156342827686702,0.0575541504231124,0.143092354725971));
#29420=CARTESIAN_POINT('',(-0.156342837828316,0.0575541228739426,0.124011319110561));
#29421=CARTESIAN_POINT('',(-0.156342830367367,0.0575541431412265,0.2));
#29422=CARTESIAN_POINT('',(-0.16659993550101,0.000146598291904576,0.0578519636609792));
#29423=CARTESIAN_POINT('Ctrl Pts',(-0.156342837828316,0.0575541228739415,
0.124011319110561));
#29424=CARTESIAN_POINT('Ctrl Pts',(-0.154725453069797,0.0619476660361069,
0.123722051905057));
#29425=CARTESIAN_POINT('Ctrl Pts',(-0.152922562753768,0.0662738589531047,
0.123429120845098));
#29426=CARTESIAN_POINT('Ctrl Pts',(-0.149942023782046,0.0726532095146394,
0.122976715419712));
#29427=CARTESIAN_POINT('Ctrl Pts',(-0.148900753953121,0.0747640516607849,
0.122823516026912));
#29428=CARTESIAN_POINT('Ctrl Pts',(-0.147120475791605,0.0781881938864711,
0.12256803993962));
#29429=CARTESIAN_POINT('Ctrl Pts',(-0.146407752373643,0.07951476552139,
0.122467290584307));
#29430=CARTESIAN_POINT('Ctrl Pts',(-0.144807331138743,0.0823990922031432,
0.12224403303186));
#29431=CARTESIAN_POINT('Ctrl Pts',(-0.143912376649387,0.083952371568136,
0.122121131200895));
#29432=CARTESIAN_POINT('Ctrl Pts',(-0.140865319360235,0.0890489022939992,
0.121709695815543));
#29433=CARTESIAN_POINT('Ctrl Pts',(-0.138606166721996,0.0925260493602986,
0.121415688135929));
#29434=CARTESIAN_POINT('Ctrl Pts',(-0.131987601239479,0.101925833718144,
0.12059029845356));
#29435=CARTESIAN_POINT('Ctrl Pts',(-0.127362172181142,0.107649781884699,
0.120052423258189));
#29436=CARTESIAN_POINT('Ctrl Pts',(-0.116462988824626,0.119447950595325,
0.118885914487657));
#29437=CARTESIAN_POINT('Ctrl Pts',(-0.11005860773267,0.125373765505653,
0.11826102472132));
#29438=CARTESIAN_POINT('Ctrl Pts',(-0.100468907855806,0.132942979895767,
0.117412556444811));
#29439=CARTESIAN_POINT('Ctrl Pts',(-0.0976505636797978,0.135026693569089,
0.117172469667474));
#29440=CARTESIAN_POINT('Ctrl Pts',(-0.0926342284172894,0.138496184859958,
0.116760554500891));
#29441=CARTESIAN_POINT('Ctrl Pts',(-0.0904657639718171,0.139922265405343,
0.116587232103598));
#29442=CARTESIAN_POINT('Ctrl Pts',(-0.0857711637345476,0.142854862961744,
0.116221519981974));
#29443=CARTESIAN_POINT('Ctrl Pts',(-0.0832366528606942,0.144346339767803,
0.116029727666112));
#29444=CARTESIAN_POINT('Ctrl Pts',(-0.0755056016015739,0.148624423514541,
0.115460033985964));
#29445=CARTESIAN_POINT('Ctrl Pts',(-0.0701991573316435,0.151203187919349,
0.115089370955084));
#29446=CARTESIAN_POINT('Ctrl Pts',(-0.0556577900395314,0.157338853934701,
0.114111547890421));
#29447=CARTESIAN_POINT('Ctrl Pts',(-0.0462251194274684,0.160363766118285,
0.113516912455412));
#29448=CARTESIAN_POINT('Ctrl Pts',(-0.0311216899010314,0.163762948705462,
0.112560746042685));
#29449=CARTESIAN_POINT('Ctrl Pts',(-0.0256054261249472,0.164715550481705,
0.112210379323951));
#29450=CARTESIAN_POINT('Ctrl Pts',(-0.018123180340744,0.165622723613347,
0.111721282727405));
#29451=CARTESIAN_POINT('Ctrl Pts',(-0.0161902152254486,0.16582283415089,
0.11159368952016));
#29452=CARTESIAN_POINT('Ctrl Pts',(-0.0127795267112629,0.166115726831495,
0.111365671898325));
#29453=CARTESIAN_POINT('Ctrl Pts',(-0.01130331371372,0.166222698840556,
0.111265992609563));
#29454=CARTESIAN_POINT('Ctrl Pts',(-0.00776304744822872,0.166431863274377,
0.111024563412211));
#29455=CARTESIAN_POINT('Ctrl Pts',(-0.00569827357786861,0.16651534067669,
0.110881892695468));
#29456=CARTESIAN_POINT('Ctrl Pts',(0.00423235326266446,0.16673192324821,
0.110188420029989));
#29457=CARTESIAN_POINT('Ctrl Pts',(0.0120988786260143,0.166346149194,0.109617582559482));
#29458=CARTESIAN_POINT('Ctrl Pts',(0.0318398590412613,0.163970172156667,
0.108170343222935));
#29459=CARTESIAN_POINT('Ctrl Pts',(0.0435834322893147,0.161246922250911,
0.107298267785005));
#29460=CARTESIAN_POINT('Ctrl Pts',(0.0580754321810927,0.156185414531604,
0.10623496321242));
#29461=CARTESIAN_POINT('Ctrl Pts',(0.0611844572555237,0.154993885334271,
0.106007371138603));
#29462=CARTESIAN_POINT('Ctrl Pts',(0.0666406373702529,0.152713019271826,
0.105608558145339));
#29463=CARTESIAN_POINT('Ctrl Pts',(0.0690019636772164,0.151660710490881,
0.105436159952716));
#29464=CARTESIAN_POINT('Ctrl Pts',(0.0740554998370496,0.149266158336814,
0.105067194513687));
#29465=CARTESIAN_POINT('Ctrl Pts',(0.0767378024219951,0.147905086639286,
0.104871352485375));
#29466=CARTESIAN_POINT('Ctrl Pts',(0.0850494095566094,0.143400531892607,
0.104262918887946));
#29467=CARTESIAN_POINT('Ctrl Pts',(0.090534187284117,0.140002459102811,
0.103859306912318));
#29468=CARTESIAN_POINT('Ctrl Pts',(0.105965446622745,0.129155020432404,
0.102694982052404));
#29469=CARTESIAN_POINT('Ctrl Pts',(0.115291283275941,0.120903114810049,
0.101955332677491));
#29470=CARTESIAN_POINT('Ctrl Pts',(0.125746101264497,0.109332513463304,
0.10096833221906));
#29471=CARTESIAN_POINT('Ctrl Pts',(0.127810701941582,0.106911654663264,
0.100764003702223));
#29472=CARTESIAN_POINT('Ctrl Pts',(0.130836062803379,0.103151307872684,
0.100447212848912));
#29473=CARTESIAN_POINT('Ctrl Pts',(0.131848437439142,0.10185409482531,0.100338030597141));
#29474=CARTESIAN_POINT('Ctrl Pts',(0.133794582534161,0.099282749825201,
0.100121330854277));
#29475=CARTESIAN_POINT('Ctrl Pts',(0.134729761177099,0.0980099255780957,
0.100013916830774));
#29476=CARTESIAN_POINT('Ctrl Pts',(0.137275900406215,0.0944391992219327,
0.0997126070083064));
#29477=CARTESIAN_POINT('Ctrl Pts',(0.138847054607245,0.0921136709067474,
0.0995164068019336));
#29478=CARTESIAN_POINT('Ctrl Pts',(0.142435093693316,0.0865023772640151,
0.0990450609108452));
#29479=CARTESIAN_POINT('Ctrl Pts',(0.144398131673898,0.0831840934769976,
0.0987679606953816));
#29480=CARTESIAN_POINT('Ctrl Pts',(0.153425932652054,0.0666396281994464,
0.0974035161330653));
#29481=CARTESIAN_POINT('Ctrl Pts',(0.158799789250376,0.0525657110113161,
0.0963033912044357));
#29482=CARTESIAN_POINT('Ctrl Pts',(0.162949719096844,0.034832132070562,
0.0950457811875245));
#29483=CARTESIAN_POINT('Ctrl Pts',(0.163591350470555,0.0316821862647794,
0.0948266727454539));
#29484=CARTESIAN_POINT('Ctrl Pts',(0.164582577603962,0.0259764547574814,
0.0944370841661147));
#29485=CARTESIAN_POINT('Ctrl Pts',(0.164964713628559,0.0234274536875381,
0.0942656232792111));
#29486=CARTESIAN_POINT('Ctrl Pts',(0.165681181264564,0.0177532588292906,
0.0938891790859353));
#29487=CARTESIAN_POINT('Ctrl Pts',(0.165986543889806,0.0146253683559193,
0.0936851661898293));
#29488=CARTESIAN_POINT('Ctrl Pts',(0.166747334164281,0.00362102136062357,
0.0929775905649838));
#29489=CARTESIAN_POINT('Ctrl Pts',(0.166731841480788,-0.00427764075400164,
0.0924884779303847));
#29490=CARTESIAN_POINT('Ctrl Pts',(0.165322441031495,-0.0235578378170679,
0.0913033146014094));
#29491=CARTESIAN_POINT('Ctrl Pts',(0.163314946520931,-0.0348518931422863,
0.0906172204000628));
#29492=CARTESIAN_POINT('Ctrl Pts',(0.159436228682321,-0.0484013730270312,
0.089717251263363));
#29493=CARTESIAN_POINT('Ctrl Pts',(0.158644994611962,-0.0509349359524964,
0.0895454300186187));
#29494=CARTESIAN_POINT('Ctrl Pts',(0.157295639567099,-0.0549185888629535,
0.0892680193261755));
#29495=CARTESIAN_POINT('Ctrl Pts',(0.156777124854499,-0.0563817569866432,
0.0891645470378549));
#29496=CARTESIAN_POINT('Ctrl Pts',(0.155654717293024,-0.0594137548381485,
0.0889464217676151));
#29497=CARTESIAN_POINT('Ctrl Pts',(0.155047393287019,-0.0609810668870776,
0.0888316053855021));
#29498=CARTESIAN_POINT('Ctrl Pts',(0.15314061379648,-0.065689152528482,
0.0884810099145395));
#29499=CARTESIAN_POINT('Ctrl Pts',(0.15176872246785,-0.0687994446702336,
0.088241652952466));
#29500=CARTESIAN_POINT('Ctrl Pts',(0.148064879562693,-0.0765458475822932,
0.0876293882844434));
#29501=CARTESIAN_POINT('Ctrl Pts',(0.145609657750549,-0.0811190339744501,
0.0872529061625451));
#29502=CARTESIAN_POINT('Ctrl Pts',(0.136553237937524,-0.0962478443415829,
0.0859697178505096));
#29503=CARTESIAN_POINT('Ctrl Pts',(0.128983760603936,-0.106177802244518,
0.0850656205665919));
#29504=CARTESIAN_POINT('Ctrl Pts',(0.118112647291995,-0.117540193372558,
0.0839774413062043));
#29505=CARTESIAN_POINT('Ctrl Pts',(0.115778188720078,-0.119840344493579,
0.0837536172618009));
#29506=CARTESIAN_POINT('Ctrl Pts',(0.111487991152771,-0.123825022607398,
0.0833590242619421));
#29507=CARTESIAN_POINT('Ctrl Pts',(0.109558157093893,-0.125535731540204,
0.0831871630467895));
#29508=CARTESIAN_POINT('Ctrl Pts',(0.105270337051431,-0.129162459165449,
0.0828168761828334));
#29509=CARTESIAN_POINT('Ctrl Pts',(0.102898067324608,-0.131060193831256,
0.082619236805612));
#29510=CARTESIAN_POINT('Ctrl Pts',(0.0950999059168477,-0.136956112569433,
0.0819906157271924));
#29511=CARTESIAN_POINT('Ctrl Pts',(0.0894827650630372,-0.140690504316021,
0.0815696259483865));
#29512=CARTESIAN_POINT('Ctrl Pts',(0.0763374955651345,-0.148323065231777,
0.0806330391153741));
#29513=CARTESIAN_POINT('Ctrl Pts',(0.0687078403585891,-0.152007807266612,
0.0801223234772568));
#29514=CARTESIAN_POINT('Ctrl Pts',(0.0554300225198149,-0.157215572582331,
0.0792426026030043));
#29515=CARTESIAN_POINT('Ctrl Pts',(0.0499221337018299,-0.159050276688578,
0.0788798991546911));
#29516=CARTESIAN_POINT('Ctrl Pts',(0.042442022341175,-0.161115090709825,
0.0783765994065113));
#29517=CARTESIAN_POINT('Ctrl Pts',(0.0405446977138068,-0.161602983684703,
0.078248029831134));
#29518=CARTESIAN_POINT('Ctrl Pts',(0.0372006286201932,-0.162400310139741,
0.0780191212582774));
#29519=CARTESIAN_POINT('Ctrl Pts',(0.0357576137834182,-0.162724122638414,
0.0779195589888421));
#29520=CARTESIAN_POINT('Ctrl Pts',(0.0323087220935698,-0.163449964455691,
0.0776797076049208));
#29521=CARTESIAN_POINT('Ctrl Pts',(0.0302995175186563,-0.16383431463467,
0.0775385346668134));
#29522=CARTESIAN_POINT('Ctrl Pts',(0.0211806703824121,-0.165405235804386,
0.0768928206973488));
#29523=CARTESIAN_POINT('Ctrl Pts',(0.0140061956319152,-0.166166541799788,
0.0763714424499903));
#29524=CARTESIAN_POINT('Ctrl Pts',(-0.00628354264827478,-0.166996086718071,
0.0748943540378242));
#29525=CARTESIAN_POINT('Ctrl Pts',(-0.0193928594358192,-0.165985577880484,
0.073941091492511));
#29526=CARTESIAN_POINT('Ctrl Pts',(-0.0354215676844072,-0.162822985381798,
0.0728124145833674));
#29527=CARTESIAN_POINT('Ctrl Pts',(-0.0385746652365065,-0.162104934439796,
0.0725919070534207));
#29528=CARTESIAN_POINT('Ctrl Pts',(-0.0442005701508189,-0.160650283112852,
0.0722008581169207));
#29529=CARTESIAN_POINT('Ctrl Pts',(-0.0466808725415322,-0.159947182789996,
0.0720293023114863));
#29530=CARTESIAN_POINT('Ctrl Pts',(-0.0521298598916357,-0.15826497675637,
0.0716538172858228));
#29531=CARTESIAN_POINT('Ctrl Pts',(-0.0550893554399453,-0.157259308702417,
0.0714508273699702));
#29532=CARTESIAN_POINT('Ctrl Pts',(-0.065206559548865,-0.153500671661056,
0.070758183119521));
#29533=CARTESIAN_POINT('Ctrl Pts',(-0.072201645883046,-0.150337263384917,
0.0702820435634966));
#29534=CARTESIAN_POINT('Ctrl Pts',(-0.08651008007617,-0.14263655597519,
0.0692849242386713));
#29535=CARTESIAN_POINT('Ctrl Pts',(-0.0937398511852317,-0.137992791231213,
0.0687668848107746));
#29536=CARTESIAN_POINT('Ctrl Pts',(-0.104304676945384,-0.129992036812475,
0.067942971452615));
#29537=CARTESIAN_POINT('Ctrl Pts',(-0.10790917241171,-0.127015738556284,
0.0676481263927458));
#29538=CARTESIAN_POINT('Ctrl Pts',(-0.112798051628228,-0.122620462677744,
0.0672206736105204));
#29539=CARTESIAN_POINT('Ctrl Pts',(-0.114190652083881,-0.121324657383668,
0.0670955428489492));
#29540=CARTESIAN_POINT('Ctrl Pts',(-0.116635044305425,-0.118970799032179,
0.0668691317276555));
#29541=CARTESIAN_POINT('Ctrl Pts',(-0.117695333627289,-0.117921975903445,
0.0667685040492619));
#29542=CARTESIAN_POINT('Ctrl Pts',(-0.12027268540814,-0.115303109619265,
0.0665179532752511));
#29543=CARTESIAN_POINT('Ctrl Pts',(-0.121773167546282,-0.113717282952366,
0.0663669053068981));
#29544=CARTESIAN_POINT('Ctrl Pts',(-0.125050274746943,-0.110114535429565,
0.0660261141656472));
#29545=CARTESIAN_POINT('Ctrl Pts',(-0.126810122722278,-0.108083177820856,
0.0658355453019171));
#29546=CARTESIAN_POINT('Ctrl Pts',(-0.132451779600306,-0.101243598795633,
0.0652012989581215));
#29547=CARTESIAN_POINT('Ctrl Pts',(-0.13611520834504,-0.0962620625635409,
0.0647511564415182));
#29548=CARTESIAN_POINT('Ctrl Pts',(-0.145131157189463,-0.0824550401687818,
0.0635516510615432));
#29549=CARTESIAN_POINT('Ctrl Pts',(-0.149956011002495,-0.0733153436261364,
0.0628074513511484));
#29550=CARTESIAN_POINT('Ctrl Pts',(-0.155250743850838,-0.0605402244058745,
0.0618471089470116));
#29551=CARTESIAN_POINT('Ctrl Pts',(-0.156493391212513,-0.0572514975734302,
0.0616063024412582));
#29552=CARTESIAN_POINT('Ctrl Pts',(-0.158473444105204,-0.0514635698880582,
0.0611931911762856));
#29553=CARTESIAN_POINT('Ctrl Pts',(-0.159257974906303,-0.0489819381026251,
0.061019387551213));
#29554=CARTESIAN_POINT('Ctrl Pts',(-0.16080711851628,-0.0436501116847052,
0.0606525674310059));
#29555=CARTESIAN_POINT('Ctrl Pts',(-0.161554811480781,-0.0407959103372634,
0.0604601530192477));
#29556=CARTESIAN_POINT('Ctrl Pts',(-0.163075217572048,-0.0342919783698597,
0.060029533881489));
#29557=CARTESIAN_POINT('Ctrl Pts',(-0.163801961467106,-0.0306330998243484,
0.0597927924426006));
#29558=CARTESIAN_POINT('Ctrl Pts',(-0.165874058716733,-0.0179937793481434,
0.0589892825605912));
#29559=CARTESIAN_POINT('Ctrl Pts',(-0.166608027402805,-0.00892999310321975,
0.0584384547184699));
#29560=CARTESIAN_POINT('Ctrl Pts',(-0.166599933793721,0.000148525849286412,
0.0578834975791045));
#29561=CARTESIAN_POINT('Ctrl Pts',(-0.16659993550101,0.000146598291904576,
0.0578519636609792));
#29562=CARTESIAN_POINT('Ctrl Pts',(-0.166590005045457,0.0114319498000848,
0.0570962429544575));
#29563=CARTESIAN_POINT('Ctrl Pts',(-0.165432367526071,0.0226678146584585,
0.0563405222479359));
#29564=CARTESIAN_POINT('Ctrl Pts',(-0.163162736528589,0.0336672156333481,
0.0555848015414142));
#29565=CARTESIAN_POINT('Ctrl Pts',(-0.161492128961394,0.0417635460604719,
0.0550285381081066));
#29566=CARTESIAN_POINT('Ctrl Pts',(-0.159212613341451,0.0497585272529405,
0.054472274674799));
#29567=CARTESIAN_POINT('Ctrl Pts',(-0.156342830367367,0.0575541431412264,
0.0539160112414913));
#29568=CARTESIAN_POINT('Ctrl Pts',(-0.156342830139253,0.0575541437608846,
0.0733422317177101));
#29569=CARTESIAN_POINT('Ctrl Pts',(-0.158731568701549,0.0510652600265771,
0.0737809469876743));
#29570=CARTESIAN_POINT('Ctrl Pts',(-0.160714366236737,0.0444330332437999,
0.0742078829840241));
#29571=CARTESIAN_POINT('Ctrl Pts',(-0.164155729589764,0.0296179894956481,
0.0751392325202815));
#29572=CARTESIAN_POINT('Ctrl Pts',(-0.165426253207922,0.0214119367621838,
0.0756406851706057));
#29573=CARTESIAN_POINT('Ctrl Pts',(-0.166428115376428,0.00875472451724462,
0.0764325626370999));
#29574=CARTESIAN_POINT('Ctrl Pts',(-0.16660137025941,0.00435192527033506,
0.0767115180698701));
#29575=CARTESIAN_POINT('Ctrl Pts',(-0.166599419703309,-0.0018801275691792,
0.0771177228895507));
#29576=CARTESIAN_POINT('Ctrl Pts',(-0.166568761872395,-0.00370787877507483,
0.077238240040562));
#29577=CARTESIAN_POINT('Ctrl Pts',(-0.166458179634013,-0.0070347046420041,
0.0774607273232043));
#29578=CARTESIAN_POINT('Ctrl Pts',(-0.166388057010376,-0.00853383941535998,
0.0775621891408969));
#29579=CARTESIAN_POINT('Ctrl Pts',(-0.166159419576139,-0.0123239897934098,
0.0778215854643722));
#29580=CARTESIAN_POINT('Ctrl Pts',(-0.16597377233047,-0.014612973676749,
0.0779808597947969));
#29581=CARTESIAN_POINT('Ctrl Pts',(-0.165040542856652,-0.0237667937472071,
0.0786264356294616));
#29582=CARTESIAN_POINT('Ctrl Pts',(-0.163913836992091,-0.0305856087662146,
0.0791265682126842));
#29583=CARTESIAN_POINT('Ctrl Pts',(-0.159519813605947,-0.0497055720309509,
0.0805538325089489));
#29584=CARTESIAN_POINT('Ctrl Pts',(-0.155262421133131,-0.0617325198928841,
0.0814780379372874));
#29585=CARTESIAN_POINT('Ctrl Pts',(-0.148236899397541,-0.076106113386055,
0.0825843105672843));
#29586=CARTESIAN_POINT('Ctrl Pts',(-0.146709724896258,-0.079009987410744,
0.0828082094017459));
#29587=CARTESIAN_POINT('Ctrl Pts',(-0.143829337061509,-0.0841150644512558,
0.0832029108509888));
#29588=CARTESIAN_POINT('Ctrl Pts',(-0.142508841221774,-0.0863333870869027,
0.083374807973937));
#29589=CARTESIAN_POINT('Ctrl Pts',(-0.139495127439928,-0.0911384725099449,
0.0837484823681112));
#29590=CARTESIAN_POINT('Ctrl Pts',(-0.137780373782819,-0.0937106311398644,
0.0839493851038715));
#29591=CARTESIAN_POINT('Ctrl Pts',(-0.131812663653349,-0.102144040124414,
0.0846129280015447));
#29592=CARTESIAN_POINT('Ctrl Pts',(-0.127249291977263,-0.107775775054225,
0.0850637453988705));
#29593=CARTESIAN_POINT('Ctrl Pts',(-0.116616450167382,-0.119277375299619,
0.0860264985571724));
#29594=CARTESIAN_POINT('Ctrl Pts',(-0.110438886896686,-0.125018934101555,
0.0865349149072511));
#29595=CARTESIAN_POINT('Ctrl Pts',(-0.0998806502011885,-0.133436262561785,
0.087370585027736));
#29596=CARTESIAN_POINT('Ctrl Pts',(-0.0957649046141287,-0.136420137754885,
0.0876894342529002));
#29597=CARTESIAN_POINT('Ctrl Pts',(-0.0899892939877273,-0.140217121976961,
0.0881371598444122));
#29598=CARTESIAN_POINT('Ctrl Pts',(-0.088442498884166,-0.141197868345446,
0.0882570987166956));
#29599=CARTESIAN_POINT('Ctrl Pts',(-0.08560925556339,-0.142929468948643,
0.088477449447536));
#29600=CARTESIAN_POINT('Ctrl Pts',(-0.084328378741345,-0.143688907055701,
0.0885773327247469));
#29601=CARTESIAN_POINT('Ctrl Pts',(-0.0813994549110805,-0.145372825718199,
0.0888065181417483));
#29602=CARTESIAN_POINT('Ctrl Pts',(-0.0797456869976875,-0.146286548653578,
0.0889364029348654));
#29603=CARTESIAN_POINT('Ctrl Pts',(-0.0737029494236593,-0.149492308915269,
0.0894117491729622));
#29604=CARTESIAN_POINT('Ctrl Pts',(-0.0692281786999842,-0.151616375908853,
0.0897651155026648));
#29605=CARTESIAN_POINT('Ctrl Pts',(-0.0546984672671851,-0.157735891793943,
0.0909031406874023));
#29606=CARTESIAN_POINT('Ctrl Pts',(-0.0443449302284133,-0.16095368818613,
0.0916983423316182));
#29607=CARTESIAN_POINT('Ctrl Pts',(-0.028043655700116,-0.164326196580587,
0.0928864723613127));
#29608=CARTESIAN_POINT('Ctrl Pts',(-0.0222762787499561,-0.165206920140448,
0.0932955254708856));
#29609=CARTESIAN_POINT('Ctrl Pts',(-0.013554452584087,-0.166073612141291,
0.0938965596568784));
#29610=CARTESIAN_POINT('Ctrl Pts',(-0.0106276164896238,-0.166286570451353,
0.0940953540341691));
#29611=CARTESIAN_POINT('Ctrl Pts',(-0.0050990113525662,-0.166542251475757,
0.0944657765890206));
#29612=CARTESIAN_POINT('Ctrl Pts',(-0.00249893778050202,-0.166601554765496,
0.0946378718472534));
#29613=CARTESIAN_POINT('Ctrl Pts',(0.00363072837520992,-0.16659781704208,
0.0950391938336234));
#29614=CARTESIAN_POINT('Ctrl Pts',(0.00715909356496179,-0.166483528040061,
0.095266759389338));
#29615=CARTESIAN_POINT('Ctrl Pts',(0.0182055568661425,-0.16577383560427,
0.0959712970743524));
#29616=CARTESIAN_POINT('Ctrl Pts',(0.0256886009519762,-0.164780211620841,
0.096436609201887));
#29617=CARTESIAN_POINT('Ctrl Pts',(0.0444685958962533,-0.16097560912945,
0.0976093198693883));
#29618=CARTESIAN_POINT('Ctrl Pts',(0.0555838564147703,-0.15748323447659,
0.0983073280844476));
#29619=CARTESIAN_POINT('Ctrl Pts',(0.0682753030885989,-0.151983370873411,
0.0991989393429221));
#29620=CARTESIAN_POINT('Ctrl Pts',(0.0702889323316825,-0.151062658622837,
0.0993434731960589));
#29621=CARTESIAN_POINT('Ctrl Pts',(0.0736272800862409,-0.149455037228192,
0.0995892598562026));
#29622=CARTESIAN_POINT('Ctrl Pts',(0.0749621564246813,-0.148789984166298,
0.0996892541357239));
#29623=CARTESIAN_POINT('Ctrl Pts',(0.0779536206656289,-0.147249119968105,
0.0999174396498739));
#29624=CARTESIAN_POINT('Ctrl Pts',(0.0796045475391126,-0.146363197318752,
0.100046182497588));
#29625=CARTESIAN_POINT('Ctrl Pts',(0.0854320084960557,-0.143108302141588,
0.10050980369882));
#29626=CARTESIAN_POINT('Ctrl Pts',(0.089520384598724,-0.140587007099171,
0.100852103650648));
#29627=CARTESIAN_POINT('Ctrl Pts',(0.101796270308284,-0.132263746396208,
0.101921751699661));
#29628=CARTESIAN_POINT('Ctrl Pts',(0.109573941582535,-0.125895777948557,
0.102658898418855));
#29629=CARTESIAN_POINT('Ctrl Pts',(0.121299019503133,-0.114381338025699,
0.103837663887317));
#29630=CARTESIAN_POINT('Ctrl Pts',(0.12560469053346,-0.109635859558593,
0.104289156339918));
#29631=CARTESIAN_POINT('Ctrl Pts',(0.131544946046503,-0.102278099295703,
0.104939686720676));
#29632=CARTESIAN_POINT('Ctrl Pts',(0.133397359197836,-0.0998500332202134,
0.10514716007322));
#29633=CARTESIAN_POINT('Ctrl Pts',(0.136692251923254,-0.0952757279756303,
0.1055253754771));
#29634=CARTESIAN_POINT('Ctrl Pts',(0.138153495069931,-0.0931442384514785,
0.105696808662908));
#29635=CARTESIAN_POINT('Ctrl Pts',(0.141383066170064,-0.0881900031280215,
0.106084984690867));
#29636=CARTESIAN_POINT('Ctrl Pts',(0.143117547028203,-0.0853464601952437,
0.106300424735804));
#29637=CARTESIAN_POINT('Ctrl Pts',(0.146640467112326,-0.0791611164753061,
0.106755206475045));
#29638=CARTESIAN_POINT('Ctrl Pts',(0.148402480185767,-0.0758064357466371,
0.106993617703762));
#29639=CARTESIAN_POINT('Ctrl Pts',(0.153470499573445,-0.065302178370474,
0.10771987981065));
#29640=CARTESIAN_POINT('Ctrl Pts',(0.156385275056003,-0.0579760350646747,
0.108198024157016));
#29641=CARTESIAN_POINT('Ctrl Pts',(0.16113041955213,-0.0430488687509527,
0.109155576867591));
#29642=CARTESIAN_POINT('Ctrl Pts',(0.162966247267559,-0.0354710286416337,
0.109633889342117));
#29643=CARTESIAN_POINT('Ctrl Pts',(0.164650804379381,-0.0255149581869932,
0.110283308696252));
#29644=CARTESIAN_POINT('Ctrl Pts',(0.164988859264248,-0.0232287635746161,
0.110433865791516));
#29645=CARTESIAN_POINT('Ctrl Pts',(0.165468015784193,-0.0194461394340785,
0.110686427201184));
#29646=CARTESIAN_POINT('Ctrl Pts',(0.165636610683883,-0.017953540089206,
0.110786988443198));
#29647=CARTESIAN_POINT('Ctrl Pts',(0.165964679388636,-0.0146489846224926,
0.111011883307279));
#29648=CARTESIAN_POINT('Ctrl Pts',(0.166114693332733,-0.0128364903485683,
0.111136659037984));
#29649=CARTESIAN_POINT('Ctrl Pts',(0.166521791127041,-0.00669660083592011,
0.111563350221079));
#29650=CARTESIAN_POINT('Ctrl Pts',(0.166639628152342,-0.00236201361199573,
0.111871273478218));
#29651=CARTESIAN_POINT('Ctrl Pts',(0.166493356417696,0.00999566398742779,
0.11275983799172));
#29652=CARTESIAN_POINT('Ctrl Pts',(0.165818805075273,0.0180020400740708,
0.113347865646239));
#29653=CARTESIAN_POINT('Ctrl Pts',(0.163340509477403,0.0337319062118775,
0.114501662729232));
#29654=CARTESIAN_POINT('Ctrl Pts',(0.161557491146787,0.0414387455357853,
0.115066166066754));
#29655=CARTESIAN_POINT('Ctrl Pts',(0.158217411307254,0.0522949462364381,
0.115854295690599));
#29656=CARTESIAN_POINT('Ctrl Pts',(0.157098191252812,0.0555668249778272,
0.116090980937147));
#29657=CARTESIAN_POINT('Ctrl Pts',(0.154962537692382,0.0612282431337444,
0.116499378285595));
#29658=CARTESIAN_POINT('Ctrl Pts',(0.153990608941746,0.0636331636134118,
0.116672496318482));
#29659=CARTESIAN_POINT('Ctrl Pts',(0.15178507890664,0.0687436173802246,
0.117040021672601));
#29660=CARTESIAN_POINT('Ctrl Pts',(0.150534400460544,0.0714408232299727,
0.11723377517437));
#29661=CARTESIAN_POINT('Ctrl Pts',(0.146484711528603,0.0795951574184007,
0.117820316762781));
#29662=CARTESIAN_POINT('Ctrl Pts',(0.143455988434335,0.0849326249752648,
0.118205144931576));
#29663=CARTESIAN_POINT('Ctrl Pts',(0.134275106575857,0.0992137338964782,
0.11925524156172));
#29664=CARTESIAN_POINT('Ctrl Pts',(0.127534271121405,0.10774117659579,0.119905035831017));
#29665=CARTESIAN_POINT('Ctrl Pts',(0.116866608477696,0.118820595415067,
0.120862540862049));
#29666=CARTESIAN_POINT('Ctrl Pts',(0.113588373994323,0.121958238504356,
0.12114923180295));
#29667=CARTESIAN_POINT('Ctrl Pts',(0.108783723971115,0.126194926374547,
0.121566149143035));
#29668=CARTESIAN_POINT('Ctrl Pts',(0.107360251990939,0.12740813774358,0.121689293944694));
#29669=CARTESIAN_POINT('Ctrl Pts',(0.104764995533598,0.129545675696416,
0.121913784456072));
#29670=CARTESIAN_POINT('Ctrl Pts',(0.103600698997363,0.130478660696752,
0.1220145340679));
#29671=CARTESIAN_POINT('Ctrl Pts',(0.100673599456555,0.13276035681628,0.122267800637389));
#29672=CARTESIAN_POINT('Ctrl Pts',(0.0988961522915688,0.134089655855697,
0.122421517376751));
#29673=CARTESIAN_POINT('Ctrl Pts',(0.0948568619017735,0.136986519536498,
0.122769725219848));
#29674=CARTESIAN_POINT('Ctrl Pts',(0.0925816622860175,0.138534345640703,
0.122965100443091));
#29675=CARTESIAN_POINT('Ctrl Pts',(0.0848292208046589,0.143532077417796,
0.123625819111869));
#29676=CARTESIAN_POINT('Ctrl Pts',(0.0791895631431683,0.146718988234542,
0.124098128204155));
#29677=CARTESIAN_POINT('Ctrl Pts',(0.0644873049629697,0.153931933053163,
0.12528975302735));
#29678=CARTESIAN_POINT('Ctrl Pts',(0.0552231197177241,0.157493213162172,
0.126003855350414));
#29679=CARTESIAN_POINT('Ctrl Pts',(0.0422968848716561,0.16118011439569,
0.126937860618442));
#29680=CARTESIAN_POINT('Ctrl Pts',(0.0388673222194977,0.162041322837214,
0.127180178827783));
#29681=CARTESIAN_POINT('Ctrl Pts',(0.0328710030423227,0.163345716702232,
0.12759474474347));
#29682=CARTESIAN_POINT('Ctrl Pts',(0.0303165747025702,0.163839044876704,
0.127768537166059));
#29683=CARTESIAN_POINT('Ctrl Pts',(0.0248607737704458,0.164760725825824,
0.128134205077161));
#29684=CARTESIAN_POINT('Ctrl Pts',(0.0219575128959662,0.16517271035205,
0.128325506240987));
#29685=CARTESIAN_POINT('Ctrl Pts',(0.0132716063530174,0.166172184108819,
0.128889417174658));
#29686=CARTESIAN_POINT('Ctrl Pts',(0.00746731810995964,0.16653401965539,
0.129255042994606));
#29687=CARTESIAN_POINT('Ctrl Pts',(-0.00791475756262302,0.166686878683553,
0.130208698672406));
#29688=CARTESIAN_POINT('Ctrl Pts',(-0.0174751900192594,0.165957145666238,
0.130785111547883));
#29689=CARTESIAN_POINT('Ctrl Pts',(-0.0327114808037987,0.163462409139054,
0.131736586375272));
#29690=CARTESIAN_POINT('Ctrl Pts',(-0.0384482258989823,0.162208878508564,
0.132102921378725));
#29691=CARTESIAN_POINT('Ctrl Pts',(-0.0458794555952046,0.16016871334915,
0.132601984904978));
#29692=CARTESIAN_POINT('Ctrl Pts',(-0.0476443715759621,0.159652605171078,
0.132722378729787));
#29693=CARTESIAN_POINT('Ctrl Pts',(-0.0508234901009825,0.158665540073413,
0.132943246903609));
#29694=CARTESIAN_POINT('Ctrl Pts',(-0.052240524163696,0.158204640056292,
0.133043181342801));
#29695=CARTESIAN_POINT('Ctrl Pts',(-0.0554341705340749,0.157118297006656,
0.133271984687267));
#29696=CARTESIAN_POINT('Ctrl Pts',(-0.05720655624845,0.156481678290817,
0.133401423888684));
#29697=CARTESIAN_POINT('Ctrl Pts',(-0.0635423209783082,0.154083932177527,
0.133872085045294));
#29698=CARTESIAN_POINT('Ctrl Pts',(-0.0680381110361262,0.152152198135693,
0.134221016081875));
#29699=CARTESIAN_POINT('Ctrl Pts',(-0.0818891571540374,0.145464030439865,
0.135330893849588));
#29700=CARTESIAN_POINT('Ctrl Pts',(-0.0908851122010791,0.140019776222052,
0.136102091463427));
#29701=CARTESIAN_POINT('Ctrl Pts',(-0.104211792718098,0.130125879207635,
0.137289251566725));
#29702=CARTESIAN_POINT('Ctrl Pts',(-0.108910971520107,0.126219086706141,
0.137718533451768));
#29703=CARTESIAN_POINT('Ctrl Pts',(-0.115560970176955,0.120041819804754,
0.138341549979697));
#29704=CARTESIAN_POINT('Ctrl Pts',(-0.117682133397078,0.117963103504322,
0.138542916082223));
#29705=CARTESIAN_POINT('Ctrl Pts',(-0.12155019648595,0.113964198452355,
0.1389155621846));
#29706=CARTESIAN_POINT('Ctrl Pts',(-0.123309959121088,0.112057771109521,
0.139087376881126));
#29707=CARTESIAN_POINT('Ctrl Pts',(-0.127313232954601,0.107512285988707,
0.139484261169915));
#29708=CARTESIAN_POINT('Ctrl Pts',(-0.129520439022757,0.104842784943497,
0.139707790081093));
#29709=CARTESIAN_POINT('Ctrl Pts',(-0.136909041057994,0.0953168511878716,
0.1404760362223));
#29710=CARTESIAN_POINT('Ctrl Pts',(-0.141642233818867,0.0881299368017429,
0.141004178464014));
#29711=CARTESIAN_POINT('Ctrl Pts',(-0.149897036826922,0.0731992596415132,
0.142046693057115));
#29712=CARTESIAN_POINT('Ctrl Pts',(-0.153420822366363,0.0654916244530294,
0.142559592849312));
#29713=CARTESIAN_POINT('Ctrl Pts',(-0.156342827686701,0.0575541504231135,
0.143092354725971));
#29714=CARTESIAN_POINT('Origin',(0.,0.,0.2));
#29715=CARTESIAN_POINT('',(-0.156342826453536,0.0575541537729419,0.213195533534746));
#29716=CARTESIAN_POINT('',(-0.156342830468371,0.0575541428668533,0.193775546749386));
#29717=CARTESIAN_POINT('',(-0.156342830367367,0.0575541431412265,0.2));
#29718=CARTESIAN_POINT('Ctrl Pts',(-0.156342830468371,0.0575541428668533,
0.193775546749386));
#29719=CARTESIAN_POINT('Ctrl Pts',(-0.155590902035664,0.0595967172780662,
0.193634523991676));
#29720=CARTESIAN_POINT('Ctrl Pts',(-0.154798947284683,0.0616245505665048,
0.193494759036807));
#29721=CARTESIAN_POINT('Ctrl Pts',(-0.149148386705545,0.0752959884263723,
0.192552560946363));
#29722=CARTESIAN_POINT('Ctrl Pts',(-0.143020724015013,0.0863702545555471,
0.191793645064661));
#29723=CARTESIAN_POINT('Ctrl Pts',(-0.131629352358015,0.102364767391474,
0.190589141621333));
#29724=CARTESIAN_POINT('Ctrl Pts',(-0.127200442878323,0.107818632368816,
0.190154220094669));
#29725=CARTESIAN_POINT('Ctrl Pts',(-0.121059808696202,0.114473725183815,
0.189567839731538));
#29726=CARTESIAN_POINT('Ctrl Pts',(-0.119650909384679,0.115945547388078,
0.1894342989407));
#29727=CARTESIAN_POINT('Ctrl Pts',(-0.117172763263459,0.11844109634221,
0.189200306920669));
#29728=CARTESIAN_POINT('Ctrl Pts',(-0.116116256578284,0.11947704506158,
0.189100780647165));
#29729=CARTESIAN_POINT('Ctrl Pts',(-0.11362150329092,0.121858906923574,
0.188866231017912));
#29730=CARTESIAN_POINT('Ctrl Pts',(-0.112173021772356,0.123193553000966,
0.188730467904189));
#29731=CARTESIAN_POINT('Ctrl Pts',(-0.106273048007432,0.128439526015559,
0.188180325182671));
#29732=CARTESIAN_POINT('Ctrl Pts',(-0.10163827341088,0.132137506705327,
0.187754626058332));
#29733=CARTESIAN_POINT('Ctrl Pts',(-0.0890019407409316,0.14116101133562,
0.186628763234608));
#29734=CARTESIAN_POINT('Ctrl Pts',(-0.0807184683879038,0.146055909391843,
0.185925283003518));
#29735=CARTESIAN_POINT('Ctrl Pts',(-0.0668126365563965,0.152726855323599,
0.184824564205049));
#29736=CARTESIAN_POINT('Ctrl Pts',(-0.0614373858124439,0.154967357349003,
0.18441629444234));
#29737=CARTESIAN_POINT('Ctrl Pts',(-0.0531950930173772,0.15790639534627,
0.183816252723021));
#29738=CARTESIAN_POINT('Ctrl Pts',(-0.050409231874744,0.158817690631178,
0.183617696139746));
#29739=CARTESIAN_POINT('Ctrl Pts',(-0.0451115338023832,0.160397181358762,
0.183247701624332));
#29740=CARTESIAN_POINT('Ctrl Pts',(-0.0426053245089632,0.161081016528133,
0.183075797932162));
#29741=CARTESIAN_POINT('Ctrl Pts',(-0.0366628688997014,0.162554044933457,
0.182674948952671));
#29742=CARTESIAN_POINT('Ctrl Pts',(-0.033215483821488,0.163293349532899,
0.182447659854307));
#29743=CARTESIAN_POINT('Ctrl Pts',(-0.0197395081635329,0.165738831654405,
0.181575877948731));
#29744=CARTESIAN_POINT('Ctrl Pts',(-0.00958645302438748,0.166634729867992,
0.18095614298273));
#29745=CARTESIAN_POINT('Ctrl Pts',(0.00689262840600602,0.166576798932987,
0.179949859274636));
#29746=CARTESIAN_POINT('Ctrl Pts',(0.0131928945247958,0.166196500623152,
0.17956456532207));
#29747=CARTESIAN_POINT('Ctrl Pts',(0.0221521436094454,0.165143004859335,
0.17899841390869));
#29748=CARTESIAN_POINT('Ctrl Pts',(0.0248399578027051,0.164760142030998,
0.178826162305901));
#29749=CARTESIAN_POINT('Ctrl Pts',(0.029684533436926,0.163948827837131,
0.178509408415356));
#29750=CARTESIAN_POINT('Ctrl Pts',(0.0318444763770192,0.163543015218502,
0.178365897848983));
#29751=CARTESIAN_POINT('Ctrl Pts',(0.0354527561390169,0.162790901329742,
0.178121344799342));
#29752=CARTESIAN_POINT('Ctrl Pts',(0.0369055734403406,0.162467701013107,
0.178021531692569));
#29753=CARTESIAN_POINT('Ctrl Pts',(0.0401827612432522,0.161692416017313,
0.177793123764577));
#29754=CARTESIAN_POINT('Ctrl Pts',(0.0420040120680982,0.161228886601921,
0.177663962869292));
#29755=CARTESIAN_POINT('Ctrl Pts',(0.0482462721053503,0.159527221104174,
0.17721447277793));
#29756=CARTESIAN_POINT('Ctrl Pts',(0.0526234378921112,0.158137292776665,
0.176887490232039));
#29757=CARTESIAN_POINT('Ctrl Pts',(0.0670704799769513,0.152883528423915,
0.175779823493162));
#29758=CARTESIAN_POINT('Ctrl Pts',(0.0768229309850354,0.14822308765669,
0.174986498453452));
#29759=CARTESIAN_POINT('Ctrl Pts',(0.09129374676517,0.139493449006873,0.173777628477773));
#29760=CARTESIAN_POINT('Ctrl Pts',(0.0963535057220681,0.136047741278424,
0.173347574493332));
#29761=CARTESIAN_POINT('Ctrl Pts',(0.103570467091752,0.130527884452616,
0.172723881325657));
#29762=CARTESIAN_POINT('Ctrl Pts',(0.105879640505845,0.128661859059181,
0.172522574862355));
#29763=CARTESIAN_POINT('Ctrl Pts',(0.110108259199288,0.12505375008256,0.172150231457662));
#29764=CARTESIAN_POINT('Ctrl Pts',(0.112039275086575,0.123326685174374,
0.171978655809551));
#29765=CARTESIAN_POINT('Ctrl Pts',(0.116448399811759,0.119194170961235,
0.17158265686525));
#29766=CARTESIAN_POINT('Ctrl Pts',(0.118893599701594,0.116755277795925,
0.171359759730468));
#29767=CARTESIAN_POINT('Ctrl Pts',(0.128937022687202,0.10609475610264,0.170426264555767));
#29768=CARTESIAN_POINT('Ctrl Pts',(0.135772186646139,0.0971946163639783,
0.169747273057942));
#29769=CARTESIAN_POINT('Ctrl Pts',(0.144689020781048,0.0827870663522616,
0.168711724052762));
#29770=CARTESIAN_POINT('Ctrl Pts',(0.147459278694621,0.0777455110692841,
0.168359194745196));
#29771=CARTESIAN_POINT('Ctrl Pts',(0.151090206733628,0.0702424552119781,
0.167834790130663));
#29772=CARTESIAN_POINT('Ctrl Pts',(0.152162694457713,0.0678878933111996,
0.167670239700088));
#29773=CARTESIAN_POINT('Ctrl Pts',(0.154014696946497,0.0635573806249942,
0.167365946902588));
#29774=CARTESIAN_POINT('Ctrl Pts',(0.15481208495677,0.0615896483756529,
0.167227074075299));
#29775=CARTESIAN_POINT('Ctrl Pts',(0.156102165787375,0.0582226140286415,
0.16698754336893));
#29776=CARTESIAN_POINT('Ctrl Pts',(0.156614147729788,0.0568310422347938,
0.166887973384925));
#29777=CARTESIAN_POINT('Ctrl Pts',(0.157739271601525,0.0536422158914378,
0.166658363647349));
#29778=CARTESIAN_POINT('Ctrl Pts',(0.158340340527467,0.0518411118861126,
0.166527716714829));
#29779=CARTESIAN_POINT('Ctrl Pts',(0.160345837373133,0.0454710750182586,
0.166063243410058));
#29780=CARTESIAN_POINT('Ctrl Pts',(0.161584218240311,0.0408526438405171,
0.165722224096999));
#29781=CARTESIAN_POINT('Ctrl Pts',(0.164917292327175,0.0258743442318358,
0.16461507909304));
#29782=CARTESIAN_POINT('Ctrl Pts',(0.166226155251371,0.015365034748537,
0.163838291744793));
#29783=CARTESIAN_POINT('Ctrl Pts',(0.166705620416753,-0.00126067209229211,
0.162648997264998));
#29784=CARTESIAN_POINT('Ctrl Pts',(0.166549233607682,-0.00732946559802726,
0.16222265838447));
#29785=CARTESIAN_POINT('Ctrl Pts',(0.165824269247632,-0.0163292683755717,
0.161602980602769));
#29786=CARTESIAN_POINT('Ctrl Pts',(0.165507737203547,-0.0192749621936129,
0.161402128481368));
#29787=CARTESIAN_POINT('Ctrl Pts',(0.164767340939304,-0.0247789865963232,
0.161030178585746));
#29788=CARTESIAN_POINT('Ctrl Pts',(0.164361987864978,-0.0273388560043736,
0.160858554083711));
#29789=CARTESIAN_POINT('Ctrl Pts',(0.163275616212723,-0.0332961300145443,
0.160461791025231));
#29790=CARTESIAN_POINT('Ctrl Pts',(0.162548009707945,-0.0366838714002988,
0.160238199069174));
#29791=CARTESIAN_POINT('Ctrl Pts',(0.159782317291051,-0.0478522076821318,
0.159505033078864));
#29792=CARTESIAN_POINT('Ctrl Pts',(0.157286713533681,-0.0555079323622843,
0.159009472486989));
#29793=CARTESIAN_POINT('Ctrl Pts',(0.151260348080733,-0.0702735030734023,
0.158034106395609));
#29794=CARTESIAN_POINT('Ctrl Pts',(0.147755980486726,-0.0773706424300446,
0.157555295301287));
#29795=CARTESIAN_POINT('Ctrl Pts',(0.141587242675839,-0.087904036955393,
0.156793263465665));
#29796=CARTESIAN_POINT('Ctrl Pts',(0.139270442342352,-0.0915303464660786,
0.156520554856046));
#29797=CARTESIAN_POINT('Ctrl Pts',(0.135781533181735,-0.0965516594783797,
0.156121854157343));
#29798=CARTESIAN_POINT('Ctrl Pts',(0.134722728798156,-0.0980236366031589,
0.156002268099135));
#29799=CARTESIAN_POINT('Ctrl Pts',(0.132744028542351,-0.100681851957852,
0.155780711342193));
#29800=CARTESIAN_POINT('Ctrl Pts',(0.131831761309077,-0.101873443162347,
0.155679223821334));
#29801=CARTESIAN_POINT('Ctrl Pts',(0.129473301841012,-0.104869302236903,
0.15541868250659));
#29802=CARTESIAN_POINT('Ctrl Pts',(0.12800545952853,-0.106656023792567,
0.155258256550875));
#29803=CARTESIAN_POINT('Ctrl Pts',(0.119362343667243,-0.116741326940189,
0.154326027947316));
#29804=CARTESIAN_POINT('Ctrl Pts',(0.111418820572436,-0.124345208204153,
0.153518728661181));
#29805=CARTESIAN_POINT('Ctrl Pts',(0.0970805142324918,-0.135585746186237,
0.152197679270653));
#29806=CARTESIAN_POINT('Ctrl Pts',(0.0910885028183082,-0.139681876623671,
0.151678087187401));
#29807=CARTESIAN_POINT('Ctrl Pts',(0.0815306895320326,-0.145338107714882,
0.150902313722887));
#29808=CARTESIAN_POINT('Ctrl Pts',(0.0781459892782143,-0.147185690476561,
0.150636877706001));
#29809=CARTESIAN_POINT('Ctrl Pts',(0.072341070658559,-0.150097615404206,
0.150196680025051));
#29810=CARTESIAN_POINT('Ctrl Pts',(0.0699542688818522,-0.151224754272853,
0.150019782273406));
#29811=CARTESIAN_POINT('Ctrl Pts',(0.0649767576493632,-0.153432242642399,
0.149658827159847));
#29812=CARTESIAN_POINT('Ctrl Pts',(0.062383500741416,-0.154504797749321,
0.149475082271993));
#29813=CARTESIAN_POINT('Ctrl Pts',(0.0551518849417202,-0.157283964654651,
0.148973432313726));
#29814=CARTESIAN_POINT('Ctrl Pts',(0.0504626632964563,-0.158850566446669,
0.148660165730293));
#29815=CARTESIAN_POINT('Ctrl Pts',(0.0342057473093257,-0.16348901522866,
0.14760408728698));
#29816=CARTESIAN_POINT('Ctrl Pts',(0.0223815903126587,-0.165522640945428,
0.146888982761485));
#29817=CARTESIAN_POINT('Ctrl Pts',(0.00530916725011301,-0.16659478022368,
0.145828901672124));
#29818=CARTESIAN_POINT('Ctrl Pts',(0.000164819562926936,-0.166679244793301,
0.1455054857326));
#29819=CARTESIAN_POINT('Ctrl Pts',(-0.00688125831788664,-0.166468755776044,
0.145047256534455));
#29820=CARTESIAN_POINT('Ctrl Pts',(-0.00878663292579114,-0.16637906309048,
0.144921806069434));
#29821=CARTESIAN_POINT('Ctrl Pts',(-0.0121719502584552,-0.166161394621268,
0.144695509294848));
#29822=CARTESIAN_POINT('Ctrl Pts',(-0.0136524385420175,-0.166046306084744,
0.144595336410489));
#29823=CARTESIAN_POINT('Ctrl Pts',(-0.0172784335945231,-0.165715614264605,
0.144347098568819));
#29824=CARTESIAN_POINT('Ctrl Pts',(-0.0194215619929738,-0.165478128081504,
0.144197947602235));
#29825=CARTESIAN_POINT('Ctrl Pts',(-0.0318903552419107,-0.163850885983391,
0.143318251045313));
#29826=CARTESIAN_POINT('Ctrl Pts',(-0.0420713689804899,-0.161536619775714,
0.142553668126449));
#29827=CARTESIAN_POINT('Ctrl Pts',(-0.0604440373342564,-0.155504501269342,
0.141148708857975));
#29828=CARTESIAN_POINT('Ctrl Pts',(-0.0686830615100061,-0.152045416485342,
0.140508302268918));
#29829=CARTESIAN_POINT('Ctrl Pts',(-0.0797162728052445,-0.146332294961448,
0.139645447249649));
#29830=CARTESIAN_POINT('Ctrl Pts',(-0.0827748121162779,-0.144624197098786,
0.139405491890529));
#29831=CARTESIAN_POINT('Ctrl Pts',(-0.0880020640675056,-0.141484737043617,
0.138993700586152));
#29832=CARTESIAN_POINT('Ctrl Pts',(-0.0901952663251361,-0.14009678561939,
0.138820374482131));
#29833=CARTESIAN_POINT('Ctrl Pts',(-0.0948036295396262,-0.137027317600559,
0.138454555610715));
#29834=CARTESIAN_POINT('Ctrl Pts',(-0.097208494089901,-0.135331904610645,
0.138262662743777));
#29835=CARTESIAN_POINT('Ctrl Pts',(-0.104302604970533,-0.13004387120222,
0.137692189543588));
#29836=CARTESIAN_POINT('Ctrl Pts',(-0.108847131272712,-0.126264620886427,
0.137320878541945));
#29837=CARTESIAN_POINT('Ctrl Pts',(-0.121052015337821,-0.114965226557501,
0.136290488975881));
#29838=CARTESIAN_POINT('Ctrl Pts',(-0.128199964147166,-0.106936194929914,
0.135647424750198));
#29839=CARTESIAN_POINT('Ctrl Pts',(-0.137436833345354,-0.0942922007309623,
0.134675459640571));
#29840=CARTESIAN_POINT('Ctrl Pts',(-0.140168561216021,-0.0901813033894219,
0.13436460105883));
#29841=CARTESIAN_POINT('Ctrl Pts',(-0.14368688933537,-0.0843397671946393,
0.133921024278536));
#29842=CARTESIAN_POINT('Ctrl Pts',(-0.144632588931071,-0.0827075082849191,
0.133796883946168));
#29843=CARTESIAN_POINT('Ctrl Pts',(-0.146274149461862,-0.0797599295986753,
0.13357171084227));
#29844=CARTESIAN_POINT('Ctrl Pts',(-0.146980452351105,-0.0784507436157472,
0.13347130949505));
#29845=CARTESIAN_POINT('Ctrl Pts',(-0.148681773339479,-0.0751935794775488,
0.133220655932239));
#29846=CARTESIAN_POINT('Ctrl Pts',(-0.149656091040029,-0.0732352193604272,
0.133069260942201));
#29847=CARTESIAN_POINT('Ctrl Pts',(-0.155630203440044,-0.0606100273830332,
0.132091473816664));
#29848=CARTESIAN_POINT('Ctrl Pts',(-0.159525009679967,-0.0494579107513059,
0.131222514451045));
#29849=CARTESIAN_POINT('Ctrl Pts',(-0.163508981470423,-0.0324465017915527,
0.129957685487496));
#29850=CARTESIAN_POINT('Ctrl Pts',(-0.164522156241036,-0.0268408734114021,
0.129549674378269));
#29851=CARTESIAN_POINT('Ctrl Pts',(-0.165801581778434,-0.0168653587799454,
0.128842252073758));
#29852=CARTESIAN_POINT('Ctrl Pts',(-0.166186499120239,-0.0125163247783635,
0.128539949306401));
#29853=CARTESIAN_POINT('Ctrl Pts',(-0.166533192612882,-0.00544373934164217,
0.128058017625432));
#29854=CARTESIAN_POINT('Ctrl Pts',(-0.166599819476558,-0.00272767396764765,
0.127875232829596));
#29855=CARTESIAN_POINT('Ctrl Pts',(-0.16660017871232,0.00268931537233102,
0.127514860709453));
#29856=CARTESIAN_POINT('Ctrl Pts',(-0.166534704148222,0.00538940658455499,
0.127337303502265));
#29857=CARTESIAN_POINT('Ctrl Pts',(-0.166196755190487,0.0123434026956459,
0.126884545791726));
#29858=CARTESIAN_POINT('Ctrl Pts',(-0.165826640331689,0.016590693821595,
0.126612434879661));
#29859=CARTESIAN_POINT('Ctrl Pts',(-0.164608846604945,0.0262592663037333,
0.125998963190014));
#29860=CARTESIAN_POINT('Ctrl Pts',(-0.16365552465737,0.0316622257808932,
0.125660532292121));
#29861=CARTESIAN_POINT('Ctrl Pts',(-0.160847749804357,0.0439860623525317,
0.12488598223878));
#29862=CARTESIAN_POINT('Ctrl Pts',(-0.15881135259047,0.0508485284896533,
0.124452809833924));
#29863=CARTESIAN_POINT('Ctrl Pts',(-0.156342837828316,0.0575541228739415,
0.124011319110561));
#29864=CARTESIAN_POINT('',(-0.166599923034401,0.00015352495594109,0.147169404797459));
#29865=CARTESIAN_POINT('Ctrl Pts',(-0.156342827686701,0.0575541504231135,
0.143092354725971));
#29866=CARTESIAN_POINT('Ctrl Pts',(-0.157207830902492,0.0552044146052684,
0.143250068585474));
#29867=CARTESIAN_POINT('Ctrl Pts',(-0.158020096597853,0.0528345395338793,
0.143409565583159));
#29868=CARTESIAN_POINT('Ctrl Pts',(-0.159414773378702,0.0484448168207871,
0.143707332104699));
#29869=CARTESIAN_POINT('Ctrl Pts',(-0.160012730606153,0.0464316190751424,
0.143844777283244));
#29870=CARTESIAN_POINT('Ctrl Pts',(-0.160967856923629,0.0429780132186727,
0.144082919624032));
#29871=CARTESIAN_POINT('Ctrl Pts',(-0.161344110448094,0.0415432095565857,
0.144182575146344));
#29872=CARTESIAN_POINT('Ctrl Pts',(-0.162172013564278,0.0382050250841271,
0.144416214233127));
#29873=CARTESIAN_POINT('Ctrl Pts',(-0.162609358618676,0.0362985059418777,
0.144550908200014));
#29874=CARTESIAN_POINT('Ctrl Pts',(-0.163513054328321,0.0320142298178966,
0.144855733414944));
#29875=CARTESIAN_POINT('Ctrl Pts',(-0.163961297132591,0.0296331167687854,
0.145026611900388));
#29876=CARTESIAN_POINT('Ctrl Pts',(-0.165841657288797,0.0182889637884391,
0.14584514452929));
#29877=CARTESIAN_POINT('Ctrl Pts',(-0.16659156282375,0.00922899163928618,
0.146510942918575));
#29878=CARTESIAN_POINT('Ctrl Pts',(-0.166599929207376,0.000153584169586965,
0.147169411303433));
#29879=CARTESIAN_POINT('Ctrl Pts',(-0.16659992926123,0.000153525741263837,
0.147169415542714));
#29880=CARTESIAN_POINT('Ctrl Pts',(-0.166605625680848,-0.00602799859208348,
0.147617917514895));
#29881=CARTESIAN_POINT('Ctrl Pts',(-0.166267281624384,-0.0122056333318352,
0.148062450528948));
#29882=CARTESIAN_POINT('Ctrl Pts',(-0.165189874066178,-0.0219275111866966,
0.148751907981414));
#29883=CARTESIAN_POINT('Ctrl Pts',(-0.164677680629216,-0.0254906855498114,
0.149002485427659));
#29884=CARTESIAN_POINT('Ctrl Pts',(-0.163531726110651,-0.0319654991952331,
0.149453920762822));
#29885=CARTESIAN_POINT('Ctrl Pts',(-0.162934544150922,-0.0348820139747416,
0.149655804269974));
#29886=CARTESIAN_POINT('Ctrl Pts',(-0.161671516362904,-0.0403063684151372,
0.15002890081508));
#29887=CARTESIAN_POINT('Ctrl Pts',(-0.161024634906989,-0.0428176456555105,
0.150200662167841));
#29888=CARTESIAN_POINT('Ctrl Pts',(-0.159397633237737,-0.0485740578146641,
0.150592686419893));
#29889=CARTESIAN_POINT('Ctrl Pts',(-0.158376565343913,-0.0518064736815498,
0.150811550875058));
#29890=CARTESIAN_POINT('Ctrl Pts',(-0.153584009957701,-0.0655080661938805,
0.151737213874922));
#29891=CARTESIAN_POINT('Ctrl Pts',(-0.148867624185716,-0.075616222069114,
0.152412634347927));
#29892=CARTESIAN_POINT('Ctrl Pts',(-0.138793270197616,-0.0925502350409985,
0.153616654347345));
#29893=CARTESIAN_POINT('Ctrl Pts',(-0.133846100035282,-0.0995705983922593,
0.154142436139106));
#29894=CARTESIAN_POINT('Ctrl Pts',(-0.12705548513444,-0.107781221067798,
0.154831617195679));
#29895=CARTESIAN_POINT('Ctrl Pts',(-0.125699785833086,-0.109359273690093,
0.154967836722193));
#29896=CARTESIAN_POINT('Ctrl Pts',(-0.123327943956184,-0.112017750412008,
0.155204698726309));
#29897=CARTESIAN_POINT('Ctrl Pts',(-0.122326312244992,-0.113110702994342,
0.155304337001842));
#29898=CARTESIAN_POINT('Ctrl Pts',(-0.119982086112629,-0.115601096559505,
0.155536751218561));
#29899=CARTESIAN_POINT('Ctrl Pts',(-0.11862954728311,-0.116988649747368,
0.155670204503956));
#29900=CARTESIAN_POINT('Ctrl Pts',(-0.113409381584476,-0.122160340888496,
0.156181801333983));
#29901=CARTESIAN_POINT('Ctrl Pts',(-0.109382668231441,-0.125778606018597,
0.156569330727374));
#29902=CARTESIAN_POINT('Ctrl Pts',(-0.0984496870463127,-0.1346800334709,
0.157589571267426));
#29903=CARTESIAN_POINT('Ctrl Pts',(-0.091292688907217,-0.139630610861674,
0.158226416037452));
#29904=CARTESIAN_POINT('Ctrl Pts',(-0.0778142376804457,-0.147472632573918,
0.159347635218781));
#29905=CARTESIAN_POINT('Ctrl Pts',(-0.0716356169777629,-0.150570889720812,
0.1598356122158));
#29906=CARTESIAN_POINT('Ctrl Pts',(-0.0624679655483101,-0.154475457779061,
0.160521188375843));
#29907=CARTESIAN_POINT('Ctrl Pts',(-0.0596215337375366,-0.15559623597791,
0.160729034718313));
#29908=CARTESIAN_POINT('Ctrl Pts',(-0.0543169627543738,-0.157517936771051,
0.161107589070845));
#29909=CARTESIAN_POINT('Ctrl Pts',(-0.0518679964467142,-0.158341229852286,
0.161278997943488));
#29910=CARTESIAN_POINT('Ctrl Pts',(-0.046281499610808,-0.160075764855271,
0.161662988426492));
#29911=CARTESIAN_POINT('Ctrl Pts',(-0.0431342859016978,-0.160952363852486,
0.161874386212139));
#29912=CARTESIAN_POINT('Ctrl Pts',(-0.0277784785747813,-0.164746613536699,
0.162885549921719));
#29913=CARTESIAN_POINT('Ctrl Pts',(-0.0152926835334805,-0.166370828963469,
0.163642668815421));
#29914=CARTESIAN_POINT('Ctrl Pts',(0.00478243539284979,-0.166701298274293,
0.164872228546539));
#29915=CARTESIAN_POINT('Ctrl Pts',(0.0123059306299837,-0.166315161011472,
0.165336848226466));
#29916=CARTESIAN_POINT('Ctrl Pts',(0.0218201068601663,-0.165177717960094,
0.165957002913224));
#29917=CARTESIAN_POINT('Ctrl Pts',(0.0238587848729861,-0.164895582018341,
0.166091833794408));
#29918=CARTESIAN_POINT('Ctrl Pts',(0.0273555759523047,-0.164345455543821,
0.166327265812509));
#29919=CARTESIAN_POINT('Ctrl Pts',(0.0288162367433764,-0.164095644057096,
0.166426905294689));
#29920=CARTESIAN_POINT('Ctrl Pts',(0.0321976072447013,-0.163470801685953,
0.166660664573319));
#29921=CARTESIAN_POINT('Ctrl Pts',(0.0341152699392348,-0.163081379671758,
0.16679549736432));
#29922=CARTESIAN_POINT('Ctrl Pts',(0.0409666040260846,-0.161563948038689,
0.167284307121912));
#29923=CARTESIAN_POINT('Ctrl Pts',(0.0458548389375537,-0.160245113937415,
0.167646260047763));
#29924=CARTESIAN_POINT('Ctrl Pts',(0.0604420331525334,-0.155587407094808,
0.168753089634216));
#29925=CARTESIAN_POINT('Ctrl Pts',(0.0699011321755486,-0.151573534196052,
0.169506030037643));
#29926=CARTESIAN_POINT('Ctrl Pts',(0.0842070112049225,-0.143877130440362,
0.170666934228259));
#29927=CARTESIAN_POINT('Ctrl Pts',(0.0893263019083245,-0.140756086154151,
0.171087778486058));
#29928=CARTESIAN_POINT('Ctrl Pts',(0.0967031956664319,-0.135693710774486,
0.17170165775218));
#29929=CARTESIAN_POINT('Ctrl Pts',(0.0990947615182789,-0.133957162504324,
0.171901977417331));
#29930=CARTESIAN_POINT('Ctrl Pts',(0.103498732515959,-0.130576851982278,
0.172273717423411));
#29931=CARTESIAN_POINT('Ctrl Pts',(0.105521308121374,-0.128947883778591,
0.172445644891415));
#29932=CARTESIAN_POINT('Ctrl Pts',(0.11017071750791,-0.125020592131762,
0.172844305624989));
#29933=CARTESIAN_POINT('Ctrl Pts',(0.112765098637182,-0.12268565847008,
0.17306945035868));
#29934=CARTESIAN_POINT('Ctrl Pts',(0.123075693176806,-0.112802541486161,
0.173979158633384));
#29935=CARTESIAN_POINT('Ctrl Pts',(0.130123044235029,-0.104594737947926,
0.17463494929481));
#29936=CARTESIAN_POINT('Ctrl Pts',(0.141356126293413,-0.0886033014285764,
0.175828828586252));
#29937=CARTESIAN_POINT('Ctrl Pts',(0.145812588780287,-0.081060171487749,
0.176364561517838));
#29938=CARTESIAN_POINT('Ctrl Pts',(0.150570586755112,-0.0713329723810846,
0.177064943667778));
#29939=CARTESIAN_POINT('Ctrl Pts',(0.151450196708202,-0.0694458885927025,
0.177201262316261));
#29940=CARTESIAN_POINT('Ctrl Pts',(0.152895273924036,-0.06618756354419,
0.177438227684291));
#29941=CARTESIAN_POINT('Ctrl Pts',(0.153478190168795,-0.0648244022885793,
0.177537867185466));
#29942=CARTESIAN_POINT('Ctrl Pts',(0.154780367724299,-0.0616631758267649,
0.177770191323627));
#29943=CARTESIAN_POINT('Ctrl Pts',(0.155486564542927,-0.0598601443253176,
0.177903550859198));
#29944=CARTESIAN_POINT('Ctrl Pts',(0.157901813076877,-0.0533623258749696,
0.178386164144234));
#29945=CARTESIAN_POINT('Ctrl Pts',(0.159430806045108,-0.0486038016221794,
0.178743240805891));
#29946=CARTESIAN_POINT('Ctrl Pts',(0.163460338477686,-0.033810320831613,
0.179850976722343));
#29947=CARTESIAN_POINT('Ctrl Pts',(0.165243092525473,-0.0236043297934682,
0.1806103537174));
#29948=CARTESIAN_POINT('Ctrl Pts',(0.16654824663301,-0.00730631698408415,
0.181778976521868));
#29949=CARTESIAN_POINT('Ctrl Pts',(0.166703470502951,-0.00129166154309381,
0.182201354869788));
#29950=CARTESIAN_POINT('Ctrl Pts',(0.166449387102815,0.00767517422182518,
0.182816897532829));
#29951=CARTESIAN_POINT('Ctrl Pts',(0.166286907649266,0.0106288788954641,
0.183017409057976));
#29952=CARTESIAN_POINT('Ctrl Pts',(0.165834303711017,0.0161642520348871,
0.183389313121233));
#29953=CARTESIAN_POINT('Ctrl Pts',(0.165562287343944,0.0187464565362648,
0.183561217882721));
#29954=CARTESIAN_POINT('Ctrl Pts',(0.164784095153417,0.0247770569001441,
0.183959542241661));
#29955=CARTESIAN_POINT('Ctrl Pts',(0.164229849752982,0.0282180760389901,
0.184184382318598));
#29956=CARTESIAN_POINT('Ctrl Pts',(0.161506393703004,0.0422976901310394,
0.18509788626771));
#29957=CARTESIAN_POINT('Ctrl Pts',(0.158407925923691,0.0527291680819541,
0.185757342828778));
#29958=CARTESIAN_POINT('Ctrl Pts',(0.15114705282707,0.0705751146936732,
0.186934433089028));
#29959=CARTESIAN_POINT('Ctrl Pts',(0.147392953926587,0.0781125058201587,
0.18744956604288));
#29960=CARTESIAN_POINT('Ctrl Pts',(0.14195214390841,0.0872356244517537,
0.188134281604874));
#29961=CARTESIAN_POINT('Ctrl Pts',(0.14077996132329,0.0891149068743666,
0.188278863129681));
#29962=CARTESIAN_POINT('Ctrl Pts',(0.138756245700188,0.0922197878926013,
0.188524708693242));
#29963=CARTESIAN_POINT('Ctrl Pts',(0.137925103827489,0.0934582821002332,
0.188624713028148));
#29964=CARTESIAN_POINT('Ctrl Pts',(0.136012709746073,0.0962268781693752,
0.188852890118991));
#29965=CARTESIAN_POINT('Ctrl Pts',(0.134922168309857,0.097750074197185,
0.18898161376892));
#29966=CARTESIAN_POINT('Ctrl Pts',(0.131217578079425,0.102744280326106,
0.189413514952243));
#29967=CARTESIAN_POINT('Ctrl Pts',(0.128493592515529,0.106131192994354,
0.189722542481169));
#29968=CARTESIAN_POINT('Ctrl Pts',(0.118428227559485,0.117689989594474,
0.190825445750196));
#29969=CARTESIAN_POINT('Ctrl Pts',(0.110414401223879,0.12523922081087,0.191633994785601));
#29970=CARTESIAN_POINT('Ctrl Pts',(0.0968345030863189,0.135707847528305,
0.192860912450915));
#29971=CARTESIAN_POINT('Ctrl Pts',(0.0917481224649588,0.139197121646909,
0.193294370168409));
#29972=CARTESIAN_POINT('Ctrl Pts',(0.0839356871501263,0.143941717437132,
0.193921893403291));
#29973=CARTESIAN_POINT('Ctrl Pts',(0.081350812955834,0.145418241016336,
0.194123764838301));
#29974=CARTESIAN_POINT('Ctrl Pts',(0.076442563281422,0.148050049664259,
0.194496850916425));
#29975=CARTESIAN_POINT('Ctrl Pts',(0.0741291190797553,0.149221840491351,
0.194668613555299));
#29976=CARTESIAN_POINT('Ctrl Pts',(0.0686756394787373,0.151825955937863,
0.195064660712538));
#29977=CARTESIAN_POINT('Ctrl Pts',(0.065516534993131,0.15321569999824,0.195287427000071));
#29978=CARTESIAN_POINT('Ctrl Pts',(0.0518930867986485,0.158710382295016,
0.196223762158694));
#29979=CARTESIAN_POINT('Ctrl Pts',(0.041071043084029,0.161848924712238,
0.196905393699765));
#29980=CARTESIAN_POINT('Ctrl Pts',(0.0243820682081625,0.164905624061368,
0.197942400090388));
#29981=CARTESIAN_POINT('Ctrl Pts',(0.0187003777396083,0.165646123699925,
0.198293591720041));
#29982=CARTESIAN_POINT('Ctrl Pts',(0.0104175768276488,0.166294027087593,
0.198816331882399));
#29983=CARTESIAN_POINT('Ctrl Pts',(0.00783873437374219,0.166435519523091,
0.198980607756016));
#29984=CARTESIAN_POINT('Ctrl Pts',(0.00313794493456894,0.166583947379469,
0.199284490054942));
#29985=CARTESIAN_POINT('Ctrl Pts',(0.00101714039397208,0.166610391570087,
0.199423231885452));
#29986=CARTESIAN_POINT('Ctrl Pts',(-0.00258791625656352,0.166586513227281,
0.19966274225901));
#29987=CARTESIAN_POINT('Ctrl Pts',(-0.00407198749604368,0.16655684403106,
0.199762429514658));
#29988=CARTESIAN_POINT('Ctrl Pts',(-0.00746008985252719,0.166443799556119,
0.199992638799527));
#29989=CARTESIAN_POINT('Ctrl Pts',(-0.00936330456397102,0.166347585073477,
0.200123777833097));
#29990=CARTESIAN_POINT('Ctrl Pts',(-0.016070824833594,0.165893028742002,
0.200591427416699));
#29991=CARTESIAN_POINT('Ctrl Pts',(-0.0208605101823373,0.165359001067689,
0.200935241265144));
#29992=CARTESIAN_POINT('Ctrl Pts',(-0.0360211930504809,0.162999514396192,
0.202042537545302));
#29993=CARTESIAN_POINT('Ctrl Pts',(-0.0462465694391194,0.16039840035885,
0.202816338009499));
#29994=CARTESIAN_POINT('Ctrl Pts',(-0.0618612298308068,0.154807762288508,
0.204002175665906));
#29995=CARTESIAN_POINT('Ctrl Pts',(-0.0674492542301364,0.152456118863135,
0.204427919311286));
#29996=CARTESIAN_POINT('Ctrl Pts',(-0.0755618554496771,0.148508406481849,
0.205047107824646));
#29997=CARTESIAN_POINT('Ctrl Pts',(-0.0781914418032904,0.147140888914951,
0.205248037889767));
#29998=CARTESIAN_POINT('Ctrl Pts',(-0.0830528163131384,0.144445573515816,
0.205620303382369));
#29999=CARTESIAN_POINT('Ctrl Pts',(-0.0852927224837764,0.143134366202129,
0.205792162078511));
#30000=CARTESIAN_POINT('Ctrl Pts',(-0.090457155303148,0.1399468801662,0.206189770569471));
#30001=CARTESIAN_POINT('Ctrl Pts',(-0.0933554888902937,0.138030365087695,
0.206413960107696));
#30002=CARTESIAN_POINT('Ctrl Pts',(-0.105159994529664,0.129682616066465,
0.207335117468991));
#30003=CARTESIAN_POINT('Ctrl Pts',(-0.113479061074266,0.122469321394276,
0.20800198532963));
#30004=CARTESIAN_POINT('Ctrl Pts',(-0.126878605028953,0.108304467259712,
0.209193402839564));
#30005=CARTESIAN_POINT('Ctrl Pts',(-0.1322457630047,0.101681178473,0.209715235239889));
#30006=CARTESIAN_POINT('Ctrl Pts',(-0.138286966326421,0.0929341981984925,
0.210402129554638));
#30007=CARTESIAN_POINT('Ctrl Pts',(-0.139457747041079,0.0911678999101304,
0.21054075441043));
#30008=CARTESIAN_POINT('Ctrl Pts',(-0.141390814187281,0.0881271867654087,
0.210780140544676));
#30009=CARTESIAN_POINT('Ctrl Pts',(-0.142170300227297,0.0868640822841078,
0.210879824105563));
#30010=CARTESIAN_POINT('Ctrl Pts',(-0.143912574579825,0.0839545568065187,
0.211110128948597));
#30011=CARTESIAN_POINT('Ctrl Pts',(-0.144864087232386,0.0823018355832543,
0.211241369910425));
#30012=CARTESIAN_POINT('Ctrl Pts',(-0.148123220865612,0.0764092385242126,
0.211709798941993));
#30013=CARTESIAN_POINT('Ctrl Pts',(-0.150274591475002,0.0720860536809101,
0.212054318696934));
#30014=CARTESIAN_POINT('Ctrl Pts',(-0.153715123657116,0.0643466838147546,
0.212665597669531));
#30015=CARTESIAN_POINT('Ctrl Pts',(-0.155085027347194,0.0609708987775182,
0.212930493239721));
#30016=CARTESIAN_POINT('Ctrl Pts',(-0.156342826453536,0.0575541537729419,
0.213195533534746));
#30017=CARTESIAN_POINT('Origin',(0.,0.,0.2));
#30018=CARTESIAN_POINT('',(-0.156342830333322,0.0575541432337077,0.283376736141222));
#30019=CARTESIAN_POINT('',(-0.156300294001537,0.0575377421133558,0.263912142181176));
#30020=CARTESIAN_POINT('',(-0.156342830367367,0.0575541431412265,0.2));
#30021=CARTESIAN_POINT('',(-0.166650872726138,-0.000148155484504217,0.197851963660979));
#30022=CARTESIAN_POINT('Ctrl Pts',(-0.15630029400153,0.0575377421133763,
0.263912142181174));
#30023=CARTESIAN_POINT('Ctrl Pts',(-0.141758267767125,0.0958745908958741,
0.261171457150951));
#30024=CARTESIAN_POINT('Ctrl Pts',(-0.0744350248633557,0.17443115827656,
0.254725118684631));
#30025=CARTESIAN_POINT('Ctrl Pts',(0.0976303930414628,0.171027438849501,
0.244573126782223));
#30026=CARTESIAN_POINT('Ctrl Pts',(0.196642115264692,0.0106749753152867,
0.233456166473938));
#30027=CARTESIAN_POINT('Ctrl Pts',(0.115571003264758,-0.159453494582782,
0.222339206165656));
#30028=CARTESIAN_POINT('Ctrl Pts',(-0.0713388377936634,-0.183556113035458,
0.211222245857374));
#30029=CARTESIAN_POINT('Ctrl Pts',(-0.160605486403313,-0.0778296844639771,
0.203059831689148));
#30030=CARTESIAN_POINT('Ctrl Pts',(-0.166754308078833,-0.0113680704511269,
0.198603070957016));
#30031=CARTESIAN_POINT('Ctrl Pts',(-0.166650872726138,-0.000148155484504217,
0.197851963660979));
#30032=CARTESIAN_POINT('Ctrl Pts',(-0.166599936070599,-0.000145949553695321,
0.197881206782592));
#30033=CARTESIAN_POINT('Ctrl Pts',(-0.166607880412107,0.00892243574673455,
0.197221034893899));
#30034=CARTESIAN_POINT('Ctrl Pts',(-0.165875392816583,0.0179775326027426,
0.196562455001654));
#30035=CARTESIAN_POINT('Ctrl Pts',(-0.163808322359624,0.0305976080986405,
0.19566088627383));
#30036=CARTESIAN_POINT('Ctrl Pts',(-0.163084763984722,0.034245342762625,
0.195402084438451));
#30037=CARTESIAN_POINT('Ctrl Pts',(-0.161569670616894,0.0407368625285207,
0.194944761351184));
#30038=CARTESIAN_POINT('Ctrl Pts',(-0.160823524757165,0.0435895199993533,
0.194744929991676));
#30039=CARTESIAN_POINT('Ctrl Pts',(-0.159279286931285,0.0489121318494712,
0.194373860417207));
#30040=CARTESIAN_POINT('Ctrl Pts',(-0.15849844211326,0.051386117030454,
0.194202122394274));
#30041=CARTESIAN_POINT('Ctrl Pts',(-0.157235648286962,0.0550838988379044,
0.193946182973806));
#30042=CARTESIAN_POINT('Ctrl Pts',(-0.156796525399903,0.0563217042233158,
0.193860636377096));
#30043=CARTESIAN_POINT('Ctrl Pts',(-0.156342830468371,0.0575541428668533,
0.193775546749386));
#30044=CARTESIAN_POINT('Ctrl Pts',(-0.156342826453536,0.0575541537729419,
0.213195533534746));
#30045=CARTESIAN_POINT('Ctrl Pts',(-0.158013874670123,0.0530148393326334,
0.213547652653047));
#30046=CARTESIAN_POINT('Ctrl Pts',(-0.159487053569706,0.0484032252857811,
0.213899981616352));
#30047=CARTESIAN_POINT('Ctrl Pts',(-0.162125560420288,0.038704199699571,
0.214625286460061));
#30048=CARTESIAN_POINT('Ctrl Pts',(-0.163256833304157,0.0336143850816674,
0.21499722941801));
#30049=CARTESIAN_POINT('Ctrl Pts',(-0.164852919071802,0.0244150085645269,
0.215651935390286));
#30050=CARTESIAN_POINT('Ctrl Pts',(-0.165406951817498,0.0203254273816211,
0.215936934039846));
#30051=CARTESIAN_POINT('Ctrl Pts',(-0.166069685598577,0.0135502970378199,
0.216399412636238));
#30052=CARTESIAN_POINT('Ctrl Pts',(-0.166266287755632,0.0108753867459279,
0.21657955244516));
#30053=CARTESIAN_POINT('Ctrl Pts',(-0.166533323150183,0.00545443404261039,
0.216940061722184));
#30054=CARTESIAN_POINT('Ctrl Pts',(-0.16660060327145,0.00270906783495527,
0.217120277603702));
#30055=CARTESIAN_POINT('Ctrl Pts',(-0.166598992421068,-0.00457385922341503,
0.217592998041431));
#30056=CARTESIAN_POINT('Ctrl Pts',(-0.166412657240988,-0.00910920072422569,
0.217881816963357));
#30057=CARTESIAN_POINT('Ctrl Pts',(-0.165545774120846,-0.0196683698132305,
0.218546558482778));
#30058=CARTESIAN_POINT('Ctrl Pts',(-0.164721301166187,-0.0256738714392414,
0.218918662560577));
#30059=CARTESIAN_POINT('Ctrl Pts',(-0.161406702268013,-0.0428196808940766,
0.219986283957887));
#30060=CARTESIAN_POINT('Ctrl Pts',(-0.158097917259412,-0.0537645505050713,
0.220673286897026));
#30061=CARTESIAN_POINT('Ctrl Pts',(-0.152906470220314,-0.0661768907999307,
0.221544216055461));
#30062=CARTESIAN_POINT('Ctrl Pts',(-0.152079948010202,-0.06805481572343,
0.221678652252109));
#30063=CARTESIAN_POINT('Ctrl Pts',(-0.150597118826183,-0.0712619372852545,
0.221913681311089));
#30064=CARTESIAN_POINT('Ctrl Pts',(-0.149957390744214,-0.0725984604713507,
0.222013324615797));
#30065=CARTESIAN_POINT('Ctrl Pts',(-0.148413218123421,-0.0757170361266824,
0.22224991952157));
#30066=CARTESIAN_POINT('Ctrl Pts',(-0.147494443597159,-0.0774915547013823,
0.222387661425436));
#30067=CARTESIAN_POINT('Ctrl Pts',(-0.143565618903204,-0.0847565765542724,
0.222963290728941));
#30068=CARTESIAN_POINT('Ctrl Pts',(-0.140279357335519,-0.0900913486878508,
0.223413879428073));
#30069=CARTESIAN_POINT('Ctrl Pts',(-0.128588364761337,-0.106873927309439,
0.224898342131217));
#30070=CARTESIAN_POINT('Ctrl Pts',(-0.119018771814515,-0.117437998868827,
0.225935915846639));
#30071=CARTESIAN_POINT('Ctrl Pts',(-0.105780308475964,-0.128749444235293,
0.227138301806463));
#30072=CARTESIAN_POINT('Ctrl Pts',(-0.103276350320605,-0.13076655159761,
0.227357458811051));
#30073=CARTESIAN_POINT('Ctrl Pts',(-0.0986609977515632,-0.134269203962835,
0.227747228535292));
#30074=CARTESIAN_POINT('Ctrl Pts',(-0.0965705438903173,-0.135780495442718,
0.227918820747597));
#30075=CARTESIAN_POINT('Ctrl Pts',(-0.0918536540908315,-0.139026497490396,
0.228295685383191));
#30076=CARTESIAN_POINT('Ctrl Pts',(-0.0892114289958802,-0.140736576083803,
0.228499981788515));
#30077=CARTESIAN_POINT('Ctrl Pts',(-0.0797437088460053,-0.146490336682967,
0.229210601248832));
#30078=CARTESIAN_POINT('Ctrl Pts',(-0.0726792989690239,-0.150120676405412,
0.229702285219482));
#30079=CARTESIAN_POINT('Ctrl Pts',(-0.0547317303879042,-0.15777860177778,
0.230898377705696));
#30080=CARTESIAN_POINT('Ctrl Pts',(-0.0436375106229962,-0.161199745833712,
0.231592576451132));
#30081=CARTESIAN_POINT('Ctrl Pts',(-0.0297796122578413,-0.16393666216094,
0.232496448752344));
#30082=CARTESIAN_POINT('Ctrl Pts',(-0.0272686370472332,-0.164372972897154,
0.232661735832045));
#30083=CARTESIAN_POINT('Ctrl Pts',(-0.0233786147963693,-0.164957328374244,
0.232921501356426));
#30084=CARTESIAN_POINT('Ctrl Pts',(-0.0220059416149619,-0.165146050923071,
0.233013872771803));
#30085=CARTESIAN_POINT('Ctrl Pts',(-0.0189933058995384,-0.165522018194618,
0.233218459816807));
#30086=CARTESIAN_POINT('Ctrl Pts',(-0.0173526398411447,-0.165702050374126,
0.233331055966956));
#30087=CARTESIAN_POINT('Ctrl Pts',(-0.0125195424540853,-0.166159830263259,
0.233665678199766));
#30088=CARTESIAN_POINT('Ctrl Pts',(-0.00932160953375049,-0.1663698668312,
0.233890836701062));
#30089=CARTESIAN_POINT('Ctrl Pts',(-0.00140443826681245,-0.166660891887333,
0.234454470469612));
#30090=CARTESIAN_POINT('Ctrl Pts',(0.00331598940546039,-0.166633804733525,
0.23479591649902));
#30091=CARTESIAN_POINT('Ctrl Pts',(0.0208649802300617,-0.165787116739579,
0.236073030885685));
#30092=CARTESIAN_POINT('Ctrl Pts',(0.033588965269019,-0.16368446200656,
0.237010029590515));
#30093=CARTESIAN_POINT('Ctrl Pts',(0.0492670428176448,-0.159186233397758,
0.238141742873034));
#30094=CARTESIAN_POINT('Ctrl Pts',(0.0525579972065923,-0.158130194544769,
0.238378300126216));
#30095=CARTESIAN_POINT('Ctrl Pts',(0.0582573777544368,-0.156103693397571,
0.238786559998225));
#30096=CARTESIAN_POINT('Ctrl Pts',(0.0606802988456382,-0.155177923028128,
0.238959665357378));
#30097=CARTESIAN_POINT('Ctrl Pts',(0.0658328096441823,-0.15307005784718,
0.239327244447322));
#30098=CARTESIAN_POINT('Ctrl Pts',(0.0685543753168823,-0.151870671619624,
0.239521062377182));
#30099=CARTESIAN_POINT('Ctrl Pts',(0.0767932179601608,-0.147973196098629,
0.240108208915414));
#30100=CARTESIAN_POINT('Ctrl Pts',(0.0821948403294156,-0.145042355729224,
0.24049355083225));
#30101=CARTESIAN_POINT('Ctrl Pts',(0.0966868869790263,-0.13610893657387,
0.241546475088437));
#30102=CARTESIAN_POINT('Ctrl Pts',(0.105368654715595,-0.129504536304905,
0.242198459367192));
#30103=CARTESIAN_POINT('Ctrl Pts',(0.116641470576333,-0.119040200006501,
0.243156359183624));
#30104=CARTESIAN_POINT('Ctrl Pts',(0.119813224956166,-0.115847251693067,
0.243440807111423));
#30105=CARTESIAN_POINT('Ctrl Pts',(0.124111378507851,-0.111154866251031,
0.243855035324084));
#30106=CARTESIAN_POINT('Ctrl Pts',(0.12534790373456,-0.109758556971357,
0.24397785581041));
#30107=CARTESIAN_POINT('Ctrl Pts',(0.1275315454847,-0.107207713437634,0.244202082635381));
#30108=CARTESIAN_POINT('Ctrl Pts',(0.12848702674732,-0.1060607006107,0.244302903427742));
#30109=CARTESIAN_POINT('Ctrl Pts',(0.130829816153224,-0.103170166138626,
0.244556842789446));
#30110=CARTESIAN_POINT('Ctrl Pts',(0.132197745273909,-0.101411433694743,
0.244711176785054));
#30111=CARTESIAN_POINT('Ctrl Pts',(0.13820263159745,-0.0933630064398376,
0.24541474726208));
#30112=CARTESIAN_POINT('Ctrl Pts',(0.142428556144468,-0.0867796302816796,
0.245982514097691));
#30113=CARTESIAN_POINT('Ctrl Pts',(0.151740976762294,-0.0697478753508089,
0.247395582125085));
#30114=CARTESIAN_POINT('Ctrl Pts',(0.15622826059357,-0.0590161254118924,
0.248236279954064));
#30115=CARTESIAN_POINT('Ctrl Pts',(0.160535351934762,-0.0446695033769497,
0.249274798940772));
#30116=CARTESIAN_POINT('Ctrl Pts',(0.161407845562433,-0.0414062075949876,
0.249505875430124));
#30117=CARTESIAN_POINT('Ctrl Pts',(0.162773567102417,-0.0355955395346767,
0.249908653138473));
#30118=CARTESIAN_POINT('Ctrl Pts',(0.163307616172096,-0.03305904395857,
0.250081610968232));
#30119=CARTESIAN_POINT('Ctrl Pts',(0.164328665052132,-0.0275780773856131,
0.25044965963089));
#30120=CARTESIAN_POINT('Ctrl Pts',(0.164796184198639,-0.0246308757122054,
0.250644075487269));
#30121=CARTESIAN_POINT('Ctrl Pts',(0.165993843992824,-0.0155025241209201,
0.251237010003819));
#30122=CARTESIAN_POINT('Ctrl Pts',(0.166457088974391,-0.00929161102473129,
0.251627280334064));
#30123=CARTESIAN_POINT('Ctrl Pts',(0.166779117532808,0.00818780566235569,
0.252707938403439));
#30124=CARTESIAN_POINT('Ctrl Pts',(0.165844937298942,0.0194356889517013,
0.253381472223035));
#30125=CARTESIAN_POINT('Ctrl Pts',(0.163043528075442,0.0344777653773826,
0.254337796592959));
#30126=CARTESIAN_POINT('Ctrl Pts',(0.162158837769444,0.0384241358473211,
0.254594292560082));
#30127=CARTESIAN_POINT('Ctrl Pts',(0.160661109801641,0.0441247747326446,
0.25497814543172));
#30128=CARTESIAN_POINT('Ctrl Pts',(0.160160847174491,0.0459074092844677,
0.255100118369454));
#30129=CARTESIAN_POINT('Ctrl Pts',(0.159207132046795,0.0491003320412027,
0.255322712968891));
#30130=CARTESIAN_POINT('Ctrl Pts',(0.158764399894478,0.0505135444543569,
0.255422754763808));
#30131=CARTESIAN_POINT('Ctrl Pts',(0.157605638394064,0.0540465396610759,
0.255676554163721));
#30132=CARTESIAN_POINT('Ctrl Pts',(0.156865662545228,0.0561580659159468,
0.255831563477038));
#30133=CARTESIAN_POINT('Ctrl Pts',(0.153178878261691,0.0660363029233616,
0.256570458931958));
#30134=CARTESIAN_POINT('Ctrl Pts',(0.149696567311978,0.0735899274956155,
0.257175312946058));
#30135=CARTESIAN_POINT('Ctrl Pts',(0.140364180784835,0.0904035553586888,
0.258575268428833));
#30136=CARTESIAN_POINT('Ctrl Pts',(0.134134987637219,0.0994121738869732,
0.259365596016227));
#30137=CARTESIAN_POINT('Ctrl Pts',(0.124817794720238,0.110400087299701,
0.26036561864635));
#30138=CARTESIAN_POINT('Ctrl Pts',(0.122485317503679,0.112982349496397,
0.260603872147409));
#30139=CARTESIAN_POINT('Ctrl Pts',(0.118274309102531,0.117360488550731,
0.261013981091134));
#30140=CARTESIAN_POINT('Ctrl Pts',(0.116431536645231,0.119188904907139,
0.261187280952365));
#30141=CARTESIAN_POINT('Ctrl Pts',(0.112396982712582,0.123009116952367,
0.261554248403444));
#30142=CARTESIAN_POINT('Ctrl Pts',(0.1101932896409,0.124987060576263,0.26174728517579));
#30143=CARTESIAN_POINT('Ctrl Pts',(0.103340215161879,0.130815867692492,
0.262327066442521));
#30144=CARTESIAN_POINT('Ctrl Pts',(0.0985330994265482,0.134473903847019,
0.262706149922257));
#30145=CARTESIAN_POINT('Ctrl Pts',(0.0849012835348428,0.143722834163063,
0.263725736413042));
#30146=CARTESIAN_POINT('Ctrl Pts',(0.0757338543323991,0.148757697181544,
0.264352065201648));
#30147=CARTESIAN_POINT('Ctrl Pts',(0.0616537990455089,0.154849711343599,
0.265303739042205));
#30148=CARTESIAN_POINT('Ctrl Pts',(0.0570681958412173,0.156597688776115,
0.265612497220262));
#30149=CARTESIAN_POINT('Ctrl Pts',(0.0505907987241755,0.1587444951795,0.266055660652341));
#30150=CARTESIAN_POINT('Ctrl Pts',(0.0487587682294856,0.159316745399522,
0.266181768875695));
#30151=CARTESIAN_POINT('Ctrl Pts',(0.0454937171895573,0.160275023181045,
0.266408550901073));
#30152=CARTESIAN_POINT('Ctrl Pts',(0.0440647293426925,0.160673770269329,
0.266508529087392));
#30153=CARTESIAN_POINT('Ctrl Pts',(0.0405971498252868,0.161591633666692,
0.266752861409693));
#30154=CARTESIAN_POINT('Ctrl Pts',(0.0385538054137087,0.162091294240902,
0.266898201692077));
#30155=CARTESIAN_POINT('Ctrl Pts',(0.0340107123621782,0.163111462585334,
0.267223543929586));
#30156=CARTESIAN_POINT('Ctrl Pts',(0.0315073503017247,0.163613456809074,
0.2674042705655));
#30157=CARTESIAN_POINT('Ctrl Pts',(0.0234756848323748,0.165032876738857,
0.267986802157955));
#30158=CARTESIAN_POINT('Ctrl Pts',(0.0179123408133515,0.165728997658714,
0.268394239156344));
#30159=CARTESIAN_POINT('Ctrl Pts',(0.000864808309352493,0.166993610074473,
0.269638653064323));
#30160=CARTESIAN_POINT('Ctrl Pts',(-0.0106542005062909,0.166655878373019,
0.27047132454534));
#30161=CARTESIAN_POINT('Ctrl Pts',(-0.0254064044734264,0.164686229793299,
0.271503396493623));
#30162=CARTESIAN_POINT('Ctrl Pts',(-0.0287505045182122,0.16413546561642,
0.271735282997761));
#30163=CARTESIAN_POINT('Ctrl Pts',(-0.0346200707000522,0.162983844976806,
0.2721389586499));
#30164=CARTESIAN_POINT('Ctrl Pts',(-0.0371525529631806,0.162425281696877,
0.272312023398853));
#30165=CARTESIAN_POINT('Ctrl Pts',(-0.042562617500353,0.161098873626916,
0.272679793213341));
#30166=CARTESIAN_POINT('Ctrl Pts',(-0.0454347579348769,0.160312532598328,
0.272873835642583));
#30167=CARTESIAN_POINT('Ctrl Pts',(-0.0541896176281827,0.157661390847867,
0.273463067168614));
#30168=CARTESIAN_POINT('Ctrl Pts',(-0.059991267237877,0.155546418960814,
0.273850176825087));
#30169=CARTESIAN_POINT('Ctrl Pts',(-0.0757855077521142,0.148773094610652,
0.274912853909615));
#30170=CARTESIAN_POINT('Ctrl Pts',(-0.0854522666934945,0.143439068563106,
0.275572390129796));
#30171=CARTESIAN_POINT('Ctrl Pts',(-0.0980605983259332,0.134752177815339,
0.276527108451761));
#30172=CARTESIAN_POINT('Ctrl Pts',(-0.101503674562533,0.132178016396924,
0.276799109988353));
#30173=CARTESIAN_POINT('Ctrl Pts',(-0.106301138027923,0.128293210937801,
0.277200808394139));
#30174=CARTESIAN_POINT('Ctrl Pts',(-0.107739063164974,0.127088053758241,
0.277324316788668));
#30175=CARTESIAN_POINT('Ctrl Pts',(-0.110282749976672,0.124881938610211,
0.277549103028597));
#30176=CARTESIAN_POINT('Ctrl Pts',(-0.111395946549046,0.12388997531534,
0.27764977294472));
#30177=CARTESIAN_POINT('Ctrl Pts',(-0.114125744409702,0.121390932981677,
0.277902295753151));
#30178=CARTESIAN_POINT('Ctrl Pts',(-0.115725881895297,0.119866438990252,
0.278055331244349));
#30179=CARTESIAN_POINT('Ctrl Pts',(-0.119237531832613,0.116384932094863,
0.278401669841419));
#30180=CARTESIAN_POINT('Ctrl Pts',(-0.121132118404769,0.114411754894627,
0.278595843742501));
#30181=CARTESIAN_POINT('Ctrl Pts',(-0.127293002899583,0.107670690581312,
0.279249867545239));
#30182=CARTESIAN_POINT('Ctrl Pts',(-0.131333102519906,0.102703927847197,
0.27971656943918));
#30183=CARTESIAN_POINT('Ctrl Pts',(-0.140944517137165,0.0893905509998384,
0.280911528153118));
#30184=CARTESIAN_POINT('Ctrl Pts',(-0.146066969095307,0.0807497519062215,
0.281634542467625));
#30185=CARTESIAN_POINT('Ctrl Pts',(-0.15190184730056,0.0685117655169172,
0.282576563831391));
#30186=CARTESIAN_POINT('Ctrl Pts',(-0.153320142551815,0.0652761089841767,
0.282818652891452));
#30187=CARTESIAN_POINT('Ctrl Pts',(-0.155225145752001,0.0605246431545676,
0.283164473075707));
#30188=CARTESIAN_POINT('Ctrl Pts',(-0.155794613410234,0.0590433459318386,
0.283270958807161));
#30189=CARTESIAN_POINT('Ctrl Pts',(-0.156342830333322,0.0575541432337077,
0.283376736141222));
#30190=CARTESIAN_POINT('Origin',(0.,0.,0.2));
#30191=CARTESIAN_POINT('',(-0.156342830367367,0.0575541431412265,0.353210893432962));
#30192=CARTESIAN_POINT('',(-0.156342830367367,0.0575541431412265,0.333924682624943));
#30193=CARTESIAN_POINT('',(-0.156342830367367,0.0575541431412265,0.2));
#30194=CARTESIAN_POINT('',(-0.166599956210055,0.000120792416194074,0.357148036344185));
#30195=CARTESIAN_POINT('Ctrl Pts',(-0.156342830367367,0.0575541431412265,
0.353210893432962));
#30196=CARTESIAN_POINT('Ctrl Pts',(-0.160082006381044,0.0473968663699324,
0.353934713614529));
#30197=CARTESIAN_POINT('Ctrl Pts',(-0.162818877487097,0.0368967108312444,
0.354658533796095));
#30198=CARTESIAN_POINT('Ctrl Pts',(-0.164515705202674,0.0262705679738153,
0.355382353977662));
#30199=CARTESIAN_POINT('Ctrl Pts',(-0.164632766007151,0.025537491291983,
0.355432288907398));
#30200=CARTESIAN_POINT('Ctrl Pts',(-0.164744897368182,0.0248038169003774,
0.355482223837133));
#30201=CARTESIAN_POINT('Ctrl Pts',(-0.164852096008479,0.0240696165655247,
0.355532158766869));
#30202=CARTESIAN_POINT('Ctrl Pts',(-0.166008400019439,0.0161501243995043,
0.356070784624253));
#30203=CARTESIAN_POINT('Ctrl Pts',(-0.166594137580341,0.0081459886045818,
0.356609410481637));
#30204=CARTESIAN_POINT('Ctrl Pts',(-0.166599956209999,0.000120792493141786,
0.357148036339021));
#30205=CARTESIAN_POINT('',(0.126907087985239,0.107935865304851,0.4));
#30206=CARTESIAN_POINT('Ctrl Pts',(-0.166599956210055,0.000120792416193977,
0.357148036344186));
#30207=CARTESIAN_POINT('Ctrl Pts',(-0.166607675272906,-0.0105255343436155,
0.357862584225541));
#30208=CARTESIAN_POINT('Ctrl Pts',(-0.165590579468026,-0.0212103033299873,
0.358577132106897));
#30209=CARTESIAN_POINT('Ctrl Pts',(-0.163552894278081,-0.0317176728853632,
0.359291679988253));
#30210=CARTESIAN_POINT('Ctrl Pts',(-0.161517022408263,-0.0422156920146834,
0.360005591999033));
#30211=CARTESIAN_POINT('Ctrl Pts',(-0.158462463953501,-0.0525356940943089,
0.360719504009813));
#30212=CARTESIAN_POINT('Ctrl Pts',(-0.154445125677035,-0.0624680970944765,
0.361433416020594));
#30213=CARTESIAN_POINT('Ctrl Pts',(-0.150429916732076,-0.0723952355694296,
0.362146949632734));
#30214=CARTESIAN_POINT('Ctrl Pts',(-0.145453298561471,-0.0819343154859597,
0.362860483244875));
#30215=CARTESIAN_POINT('Ctrl Pts',(-0.13961945659845,-0.0908953647836543,
0.363574016857016));
#30216=CARTESIAN_POINT('Ctrl Pts',(-0.133772930661803,-0.099875897247618,
0.364289101838147));
#30217=CARTESIAN_POINT('Ctrl Pts',(-0.127066019493771,-0.108275133680505,
0.365004186819279));
#30218=CARTESIAN_POINT('Ctrl Pts',(-0.119645261781961,-0.115933478051536,
0.36571927180041));
#30219=CARTESIAN_POINT('Ctrl Pts',(-0.11642878098275,-0.119252939295227,
0.36602922089199));
#30220=CARTESIAN_POINT('Ctrl Pts',(-0.113078664409795,-0.122433674563659,
0.366339169983571));
#30221=CARTESIAN_POINT('Ctrl Pts',(-0.109608799634176,-0.125465019199596,
0.366649119075151));
#30222=CARTESIAN_POINT('Ctrl Pts',(-0.101483921909479,-0.132563078086924,
0.367374881787193));
#30223=CARTESIAN_POINT('Ctrl Pts',(-0.0926376574341541,-0.138894029613974,
0.368100644499235));
#30224=CARTESIAN_POINT('Ctrl Pts',(-0.0832388006807538,-0.144315148412181,
0.368826407211277));
#30225=CARTESIAN_POINT('Ctrl Pts',(-0.0735911687511109,-0.149879756979392,
0.36957137989229));
#30226=CARTESIAN_POINT('Ctrl Pts',(-0.0633619535574521,-0.154484921721223,
0.370316352573303));
#30227=CARTESIAN_POINT('Ctrl Pts',(-0.0527670590063455,-0.158022775206047,
0.371061325254316));
#30228=CARTESIAN_POINT('Ctrl Pts',(-0.0424682753811155,-0.16146175115453,
0.37178547710042));
#30229=CARTESIAN_POINT('Ctrl Pts',(-0.0318249391874584,-0.163892136062298,
0.372509628946524));
#30230=CARTESIAN_POINT('Ctrl Pts',(-0.0210538606503979,-0.165264318446886,
0.373233780792628));
#30231=CARTESIAN_POINT('Ctrl Pts',(-0.0098182465689913,-0.16669568037313,
0.373989163891096));
#30232=CARTESIAN_POINT('Ctrl Pts',(0.00155535427931255,-0.166975096912089,
0.374744546989564));
#30233=CARTESIAN_POINT('Ctrl Pts',(0.0128153468683916,-0.166106372197585,
0.375499930088031));
#30234=CARTESIAN_POINT('Ctrl Pts',(0.0240753394574707,-0.165237647483082,
0.376255313186499));
#30235=CARTESIAN_POINT('Ctrl Pts',(0.0352206347865155,-0.163221015343348,
0.377010696284967));
#30236=CARTESIAN_POINT('Ctrl Pts',(0.0460104551749553,-0.160120573364554,
0.377766079383434));
#30237=CARTESIAN_POINT('Ctrl Pts',(0.0562505702150188,-0.157178088559903,
0.378482978233383));
#30238=CARTESIAN_POINT('Ctrl Pts',(0.0662497085449184,-0.153236917219443,
0.379199877083332));
#30239=CARTESIAN_POINT('Ctrl Pts',(0.0757999579594132,-0.148357427766025,
0.379916775933281));
#30240=CARTESIAN_POINT('Ctrl Pts',(0.085753716337752,-0.143271774300759,
0.380663964579818));
#30241=CARTESIAN_POINT('Ctrl Pts',(0.0952186826030546,-0.13716680807782,
0.381411153226354));
#30242=CARTESIAN_POINT('Ctrl Pts',(0.103980953453111,-0.130167282060363,
0.38215834187289));
#30243=CARTESIAN_POINT('Ctrl Pts',(0.112369982262007,-0.123465911329659,
0.382873702900726));
#30244=CARTESIAN_POINT('Ctrl Pts',(0.120114332795534,-0.115945468949997,
0.383589063928562));
#30245=CARTESIAN_POINT('Ctrl Pts',(0.127057953112165,-0.10775823194052,
0.384304424956398));
#30246=CARTESIAN_POINT('Ctrl Pts',(0.134002789498536,-0.099569561060709,
0.385019911268864));
#30247=CARTESIAN_POINT('Ctrl Pts',(0.140146049725854,-0.0907146042217684,
0.385735397581329));
#30248=CARTESIAN_POINT('Ctrl Pts',(0.145372698665044,-0.0813777517681734,
0.386450883893795));
#30249=CARTESIAN_POINT('Ctrl Pts',(0.150613002558104,-0.0720165061917496,
0.387168239459907));
#30250=CARTESIAN_POINT('Ctrl Pts',(0.154931550656227,-0.0621717109485352,
0.38788559502602));
#30251=CARTESIAN_POINT('Ctrl Pts',(0.1582606550982,-0.0520492559782427,
0.388602950592133));
#30252=CARTESIAN_POINT('Ctrl Pts',(0.158693934357758,-0.0507318296640838,
0.388696313625327));
#30253=CARTESIAN_POINT('Ctrl Pts',(0.159110524094924,-0.0494097169799387,
0.388789676658522));
#30254=CARTESIAN_POINT('Ctrl Pts',(0.159510338674996,-0.0480833844044693,
0.388883039691717));
#30255=CARTESIAN_POINT('Ctrl Pts',(0.162700330881156,-0.0375010024969307,
0.389627953366905));
#30256=CARTESIAN_POINT('Ctrl Pts',(0.164842651460865,-0.0265681615428049,
0.390372867042094));
#30257=CARTESIAN_POINT('Ctrl Pts',(0.165876691278507,-0.0155075236738458,
0.391117780717282));
#30258=CARTESIAN_POINT('Ctrl Pts',(0.166908350772131,-0.00447234701201396,
0.391860979626866));
#30259=CARTESIAN_POINT('Ctrl Pts',(0.166836640415639,0.00668921134358856,
0.39260417853645));
#30260=CARTESIAN_POINT('Ctrl Pts',(0.165652190126399,0.017745757417684,
0.393347377446034));
#30261=CARTESIAN_POINT('Ctrl Pts',(0.164469606478383,0.0287848788646129,
0.394089405107036));
#30262=CARTESIAN_POINT('Ctrl Pts',(0.162177817279617,0.0397184708520597,
0.394831432768038));
#30263=CARTESIAN_POINT('Ctrl Pts',(0.158819395386297,0.0503185815492748,
0.395573460429041));
#30264=CARTESIAN_POINT('Ctrl Pts',(0.155458738367561,0.0609257469220445,
0.396315981930584));
#30265=CARTESIAN_POINT('Ctrl Pts',(0.15103026034291,0.0711981668756874,
0.397058503432127));
#30266=CARTESIAN_POINT('Ctrl Pts',(0.145626686853412,0.0809223583201725,
0.39780102493367));
#30267=CARTESIAN_POINT('Ctrl Pts',(0.140292464949716,0.0905217456699905,
0.398534016622447));
#30268=CARTESIAN_POINT('Ctrl Pts',(0.134008531813893,0.0995862444050702,
0.399267008311223));
#30269=CARTESIAN_POINT('Ctrl Pts',(0.126907087985239,0.10793586530485,0.4));
#30270=CARTESIAN_POINT('',(-0.126912151695562,0.107929911294333,0.399999950528882));
#30271=CARTESIAN_POINT('Origin',(0.,0.,0.4));
#30272=CARTESIAN_POINT('',(-0.166599974196028,9.27247699980398E-5,0.337851963656908));
#30273=CARTESIAN_POINT('Ctrl Pts',(-0.126912151695562,0.107929911294333,
0.399999950528882));
#30274=CARTESIAN_POINT('Ctrl Pts',(-0.119947535241094,0.116119434007461,
0.399276600529823));
#30275=CARTESIAN_POINT('Ctrl Pts',(-0.112160840526412,0.123662698151552,
0.398553250530764));
#30276=CARTESIAN_POINT('Ctrl Pts',(-0.103696444166919,0.130394046900681,
0.397829900531706));
#30277=CARTESIAN_POINT('Ctrl Pts',(-0.0951773525351325,0.137168892307706,
0.397101876386555));
#30278=CARTESIAN_POINT('Ctrl Pts',(-0.085972380799809,0.14312057361781,
0.396373852241404));
#30279=CARTESIAN_POINT('Ctrl Pts',(-0.0762661277144263,0.148118323523617,
0.395645828096254));
#30280=CARTESIAN_POINT('Ctrl Pts',(-0.0666443076806357,0.153072598849487,
0.394924136909832));
#30281=CARTESIAN_POINT('Ctrl Pts',(-0.0565307295261072,0.157089069983039,
0.394202445723411));
#30282=CARTESIAN_POINT('Ctrl Pts',(-0.0461308220115868,0.160085937110464,
0.39348075453699));
#30283=CARTESIAN_POINT('Ctrl Pts',(-0.0355940231514617,0.163122251239998,
0.392749563912475));
#30284=CARTESIAN_POINT('Ctrl Pts',(-0.0247642098773763,0.165111604793141,
0.39201837328796));
#30285=CARTESIAN_POINT('Ctrl Pts',(-0.0138683517813452,0.166021772123023,
0.391287182663444));
#30286=CARTESIAN_POINT('Ctrl Pts',(-0.00297249368531417,0.166931939452904,
0.390555992038929));
#30287=CARTESIAN_POINT('Ctrl Pts',(0.007988440041223,0.166762970969527,
0.389824801414414));
#30288=CARTESIAN_POINT('Ctrl Pts',(0.0187884890345102,0.165537164044211,
0.389093610789898));
#30289=CARTESIAN_POINT('Ctrl Pts',(0.0295122497374452,0.164320015849489,
0.388367585075533));
#30290=CARTESIAN_POINT('Ctrl Pts',(0.0401551997329114,0.162052204061964,
0.387641559361168));
#30291=CARTESIAN_POINT('Ctrl Pts',(0.0504980366376883,0.158762427216702,
0.386915533646802));
#30292=CARTESIAN_POINT('Ctrl Pts',(0.0611098520847941,0.155387095567805,
0.38617062671637));
#30293=CARTESIAN_POINT('Ctrl Pts',(0.0714047096220906,0.150935892100486,
0.385425719785938));
#30294=CARTESIAN_POINT('Ctrl Pts',(0.0811576670828012,0.145495680601443,
0.384680812855506));
#30295=CARTESIAN_POINT('Ctrl Pts',(0.0906427759753403,0.140204875358548,
0.383956363540678));
#30296=CARTESIAN_POINT('Ctrl Pts',(0.0996146075556019,0.133979282411873,
0.38323191422585));
#30297=CARTESIAN_POINT('Ctrl Pts',(0.107890355537113,0.126945780481572,
0.382507464911022));
#30298=CARTESIAN_POINT('Ctrl Pts',(0.116516649928662,0.119614351541268,
0.381752329172788));
#30299=CARTESIAN_POINT('Ctrl Pts',(0.124385600621863,0.111405537080788,
0.380997193434553));
#30300=CARTESIAN_POINT('Ctrl Pts',(0.131330797395314,0.102507471218009,
0.380242057696319));
#30301=CARTESIAN_POINT('Ctrl Pts',(0.138275994168766,0.0936094053552298,
0.379486921958085));
#30302=CARTESIAN_POINT('Ctrl Pts',(0.144296878889521,0.0840230462814757,
0.37873178621985));
#30303=CARTESIAN_POINT('Ctrl Pts',(0.149278728771727,0.0739690552616248,
0.377976650481616));
#30304=CARTESIAN_POINT('Ctrl Pts',(0.154053604917181,0.0643327629159306,
0.377252887279526));
#30305=CARTESIAN_POINT('Ctrl Pts',(0.157909601642383,0.0541957456425725,
0.376529124077436));
#30306=CARTESIAN_POINT('Ctrl Pts',(0.160751247714667,0.0437561008109459,
0.375805360875347));
#30307=CARTESIAN_POINT('Ctrl Pts',(0.163678129271707,0.0330033176907131,
0.375059888316845));
#30308=CARTESIAN_POINT('Ctrl Pts',(0.165528232910599,0.0219303145823395,
0.374314415758344));
#30309=CARTESIAN_POINT('Ctrl Pts',(0.166251225055711,0.0107745147211016,
0.373568943199843));
#30310=CARTESIAN_POINT('Ctrl Pts',(0.166951509711302,-3.09076012234098E-5,
0.372846884187984));
#30311=CARTESIAN_POINT('Ctrl Pts',(0.166594543597082,-0.0109130254897179,
0.372124825176124));
#30312=CARTESIAN_POINT('Ctrl Pts',(0.165187201660095,-0.0216505983221526,
0.371402766164264));
#30313=CARTESIAN_POINT('Ctrl Pts',(0.163711407839935,-0.0329104373230026,
0.370645586832442));
#30314=CARTESIAN_POINT('Ctrl Pts',(0.161080294950841,-0.0440101868140574,
0.36988840750062));
#30315=CARTESIAN_POINT('Ctrl Pts',(0.15736244965134,-0.0547048392715816,
0.369131228168798));
#30316=CARTESIAN_POINT('Ctrl Pts',(0.153644604351838,-0.0653994917291058,
0.368374048836976));
#30317=CARTESIAN_POINT('Ctrl Pts',(0.148840548557795,-0.0756880211301988,
0.367616869505155));
#30318=CARTESIAN_POINT('Ctrl Pts',(0.143075557820479,-0.0853518878195371,
0.366859690173333));
#30319=CARTESIAN_POINT('Ctrl Pts',(0.137555879679565,-0.0946045364624177,
0.366134730429762));
#30320=CARTESIAN_POINT('Ctrl Pts',(0.131114667484915,-0.103353509144416,
0.365409770686192));
#30321=CARTESIAN_POINT('Ctrl Pts',(0.12386750309171,-0.111410958517667,
0.364684810942622));
#30322=CARTESIAN_POINT('Ctrl Pts',(0.116418269742169,-0.119693069606485,
0.363939637519491));
#30323=CARTESIAN_POINT('Ctrl Pts',(0.108117869668668,-0.127243570141914,
0.36319446409636));
#30324=CARTESIAN_POINT('Ctrl Pts',(0.0991382592325092,-0.13389236556409,
0.362449290673229));
#30325=CARTESIAN_POINT('Ctrl Pts',(0.0904222880731206,-0.140345953896943,
0.361725995368724));
#30326=CARTESIAN_POINT('Ctrl Pts',(0.0810673064246538,-0.145949611427857,
0.36100270006422));
#30327=CARTESIAN_POINT('Ctrl Pts',(0.0712635883715059,-0.15058904665485,
0.360279404759715));
#30328=CARTESIAN_POINT('Ctrl Pts',(0.0610150584167484,-0.155438981204093,
0.359523292277271));
#30329=CARTESIAN_POINT('Ctrl Pts',(0.0502769557916214,-0.159234397099614,
0.358767179794827));
#30330=CARTESIAN_POINT('Ctrl Pts',(0.0392907384715136,-0.161900580203911,
0.358011067312383));
#30331=CARTESIAN_POINT('Ctrl Pts',(0.0283045211514057,-0.164566763308208,
0.357254954829938));
#30332=CARTESIAN_POINT('Ctrl Pts',(0.0170713121684996,-0.166103596998203,
0.356498842347494));
#30333=CARTESIAN_POINT('Ctrl Pts',(0.00584102204421006,-0.166497574941736,
0.35574272986505));
#30334=CARTESIAN_POINT('Ctrl Pts',(-0.0049256806434658,-0.166875289438564,
0.355017829777267));
#30335=CARTESIAN_POINT('Ctrl Pts',(-0.0157686683437115,-0.166205706831982,
0.354292929689485));
#30336=CARTESIAN_POINT('Ctrl Pts',(-0.0264674582994453,-0.164484144072209,
0.353568029601703));
#30337=CARTESIAN_POINT('Ctrl Pts',(-0.0374656822343477,-0.162714398817996,
0.352822841264625));
#30338=CARTESIAN_POINT('Ctrl Pts',(-0.0483105010955349,-0.159832727950378,
0.352077652927547));
#30339=CARTESIAN_POINT('Ctrl Pts',(-0.0587657332681133,-0.155891464145607,
0.351332464590469));
#30340=CARTESIAN_POINT('Ctrl Pts',(-0.0689131274043697,-0.15206624471845,
0.350609217163988));
#30341=CARTESIAN_POINT('Ctrl Pts',(-0.0786927167223967,-0.147243454704251,
0.349885969737508));
#30342=CARTESIAN_POINT('Ctrl Pts',(-0.0879053564862984,-0.141521052501092,
0.349162722311028));
#30343=CARTESIAN_POINT('Ctrl Pts',(-0.0975372173176259,-0.135538252450918,
0.348406563518651));
#30344=CARTESIAN_POINT('Ctrl Pts',(-0.106548233235344,-0.128572340363373,
0.347650404726274));
#30345=CARTESIAN_POINT('Ctrl Pts',(-0.114744722882249,-0.12078579622901,
0.346894245933897));
#30346=CARTESIAN_POINT('Ctrl Pts',(-0.122941212529154,-0.112999252094647,
0.34613808714152));
#30347=CARTESIAN_POINT('Ctrl Pts',(-0.130322469069809,-0.104392957478539,
0.345381928349144));
#30348=CARTESIAN_POINT('Ctrl Pts',(-0.136741702362345,-0.0951696739252992,
0.344625769556767));
#30349=CARTESIAN_POINT('Ctrl Pts',(-0.14296702617097,-0.0862250034201091,
0.343892452489329));
#30350=CARTESIAN_POINT('Ctrl Pts',(-0.148333340221089,-0.0766351629444054,
0.34315913542189));
#30351=CARTESIAN_POINT('Ctrl Pts',(-0.15271467922135,-0.0665866859839123,
0.342425818354452));
#30352=CARTESIAN_POINT('Ctrl Pts',(-0.157269236597204,-0.0561409375828448,
0.341663509238873));
#30353=CARTESIAN_POINT('Ctrl Pts',(-0.160758522692059,-0.0452002413067621,
0.340901200123295));
#30354=CARTESIAN_POINT('Ctrl Pts',(-0.163092875949299,-0.0340040264466811,
0.340138891007716));
#30355=CARTESIAN_POINT('Ctrl Pts',(-0.165427229206539,-0.0228078115866,
0.339376581892137));
#30356=CARTESIAN_POINT('Ctrl Pts',(-0.166606346848609,-0.011357122512868,
0.338614272776558));
#30357=CARTESIAN_POINT('Ctrl Pts',(-0.166599974196062,9.27247088470251E-5,
0.337851963660979));
#30358=CARTESIAN_POINT('Ctrl Pts',(-0.166599974196028,9.27247699982471E-5,
0.337851963656908));
#30359=CARTESIAN_POINT('Ctrl Pts',(-0.166593228454842,0.0122128983487723,
0.337045025483611));
#30360=CARTESIAN_POINT('Ctrl Pts',(-0.165259685224493,0.0242846265757986,
0.336238087310314));
#30361=CARTESIAN_POINT('Ctrl Pts',(-0.162655324506395,0.0360389429606284,
0.335431149137018));
#30362=CARTESIAN_POINT('Ctrl Pts',(-0.161034637677667,0.0433536231480551,
0.334928993632993));
#30363=CARTESIAN_POINT('Ctrl Pts',(-0.158922840566651,0.0505456798939685,
0.334426838128968));
#30364=CARTESIAN_POINT('Ctrl Pts',(-0.156342830367367,0.0575541431412263,
0.333924682624943));
#30365=CARTESIAN_POINT('Origin',(0.,0.,0.2));
#30366=CARTESIAN_POINT('',(-0.166599975890259,8.9629041933745E-5,0.267851966777163));
#30367=CARTESIAN_POINT('Ctrl Pts',(-0.156342830367367,0.0575541431412263,
0.333924682624943));
#30368=CARTESIAN_POINT('Ctrl Pts',(-0.155630595781153,0.0594888912760559,
0.333786058166124));
#30369=CARTESIAN_POINT('Ctrl Pts',(-0.154882719734524,0.0614096680351601,
0.333647433707304));
#30370=CARTESIAN_POINT('Ctrl Pts',(-0.154099774838887,0.0633152382496057,
0.333508809248485));
#30371=CARTESIAN_POINT('Ctrl Pts',(-0.150006198854086,0.0732783870109964,
0.332784020366546));
#30372=CARTESIAN_POINT('Ctrl Pts',(-0.144927306279316,0.0828795908971444,
0.332059231484606));
#30373=CARTESIAN_POINT('Ctrl Pts',(-0.1389496178186,0.0919160688240363,
0.331334442602667));
#30374=CARTESIAN_POINT('Ctrl Pts',(-0.132803455780128,0.10120722843544,
0.330589226464128));
#30375=CARTESIAN_POINT('Ctrl Pts',(-0.125707325343765,0.109900349908042,
0.329844010325589));
#30376=CARTESIAN_POINT('Ctrl Pts',(-0.117806257442659,0.117801722005045,
0.329098794187051));
#30377=CARTESIAN_POINT('Ctrl Pts',(-0.11013940500608,0.125468869620085,
0.328375668878036));
#30378=CARTESIAN_POINT('Ctrl Pts',(-0.101715466852179,0.132389988772537,
0.327652543569021));
#30379=CARTESIAN_POINT('Ctrl Pts',(-0.092705710586656,0.138424026905098,
0.326929418260006));
#30380=CARTESIAN_POINT('Ctrl Pts',(-0.083283094363323,0.144734566715996,
0.326173156706705));
#30381=CARTESIAN_POINT('Ctrl Pts',(-0.0732204191893915,0.150073934404664,
0.325416895153405));
#30382=CARTESIAN_POINT('Ctrl Pts',(-0.0627457002634819,0.154332553592705,
0.324660633600104));
#30383=CARTESIAN_POINT('Ctrl Pts',(-0.0522709813375724,0.158591172780747,
0.323904372046803));
#30384=CARTESIAN_POINT('Ctrl Pts',(-0.0413853152555228,0.161768762188444,
0.323148110493502));
#30385=CARTESIAN_POINT('Ctrl Pts',(-0.0303341135834924,0.163815144455889,
0.322391848940202));
#30386=CARTESIAN_POINT('Ctrl Pts',(-0.0197431633200151,0.165776300668378,
0.321667083549533));
#30387=CARTESIAN_POINT('Ctrl Pts',(-0.00892221477796013,0.166713339777031,
0.320942318158864));
#30388=CARTESIAN_POINT('Ctrl Pts',(0.00191144223773458,0.166589034418751,
0.320217552768195));
#30389=CARTESIAN_POINT('Ctrl Pts',(0.0130508809796042,0.166461220521575,
0.319472330756839));
#30390=CARTESIAN_POINT('Ctrl Pts',(0.0242027780835187,0.165210915452516,
0.318727108745483));
#30391=CARTESIAN_POINT('Ctrl Pts',(0.0351257177818648,0.16285497827917,
0.317981886734126));
#30392=CARTESIAN_POINT('Ctrl Pts',(0.0457244496428421,0.160568968553657,
0.317258783934569));
#30393=CARTESIAN_POINT('Ctrl Pts',(0.0561067201092357,0.157242405567947,
0.316535681135013));
#30394=CARTESIAN_POINT('Ctrl Pts',(0.0660611681537217,0.152942741122832,
0.315812578335456));
#30395=CARTESIAN_POINT('Ctrl Pts',(0.0764723656633846,0.148445791059573,
0.3150562967182));
#30396=CARTESIAN_POINT('Ctrl Pts',(0.0864144302980466,0.14288445654869,
0.314300015100943));
#30397=CARTESIAN_POINT('Ctrl Pts',(0.0956716550808264,0.136390961629044,
0.313543733483687));
#30398=CARTESIAN_POINT('Ctrl Pts',(0.104928879863606,0.129897466709398,
0.312787451866431));
#30399=CARTESIAN_POINT('Ctrl Pts',(0.11350043373518,0.122472580726663,0.312031170249175));
#30400=CARTESIAN_POINT('Ctrl Pts',(0.12121110516053,0.114295354174013,0.311274888631919));
#30401=CARTESIAN_POINT('Ctrl Pts',(0.128600073795149,0.106459295913629,
0.310550160415583));
#30402=CARTESIAN_POINT('Ctrl Pts',(0.135253270227448,0.097874840020428,
0.309825432199247));
#30403=CARTESIAN_POINT('Ctrl Pts',(0.141021614388083,0.0887043644663494,
0.309100703982911));
#30404=CARTESIAN_POINT('Ctrl Pts',(0.146953149202477,0.0792744494857578,
0.308355472677972));
#30405=CARTESIAN_POINT('Ctrl Pts',(0.151948200500906,0.0692254989172822,
0.307610241373032));
#30406=CARTESIAN_POINT('Ctrl Pts',(0.155890032973563,0.0587695296858969,
0.306865010068092));
#30407=CARTESIAN_POINT('Ctrl Pts',(0.159714609240943,0.0486245902314157,
0.306141946877977));
#30408=CARTESIAN_POINT('Ctrl Pts',(0.162547562502924,0.0380974657469978,
0.305418883687861));
#30409=CARTESIAN_POINT('Ctrl Pts',(0.164330987445657,0.0274023094854309,
0.304695820497745));
#30410=CARTESIAN_POINT('Ctrl Pts',(0.166196428392214,0.0162153052319293,
0.303939505135394));
#30411=CARTESIAN_POINT('Ctrl Pts',(0.166913020611866,0.00484546047150204,
0.303183189773042));
#30412=CARTESIAN_POINT('Ctrl Pts',(0.166474931774067,-0.00645423045915291,
0.30242687441069));
#30413=CARTESIAN_POINT('Ctrl Pts',(0.166036842936267,-0.017753921389808,
0.301670559048339));
#30414=CARTESIAN_POINT('Ctrl Pts',(0.164444269118064,-0.0289823423839235,
0.300914243685987));
#30415=CARTESIAN_POINT('Ctrl Pts',(0.161752704107014,-0.0398951464976462,
0.300157928323636));
#30416=CARTESIAN_POINT('Ctrl Pts',(0.15917345289749,-0.050352580404712,
0.299433172538388));
#30417=CARTESIAN_POINT('Ctrl Pts',(0.155566370516096,-0.0605973979856725,
0.298708416753141));
#30418=CARTESIAN_POINT('Ctrl Pts',(0.150987106295862,-0.0704162888286652,
0.297983660967894));
#30419=CARTESIAN_POINT('Ctrl Pts',(0.146278514024313,-0.0805124857972116,
0.297238436555182));
#30420=CARTESIAN_POINT('Ctrl Pts',(0.140542100949058,-0.090157307397608,
0.29649321214247));
#30421=CARTESIAN_POINT('Ctrl Pts',(0.133892745257038,-0.0991377464315882,
0.295747987729758));
#30422=CARTESIAN_POINT('Ctrl Pts',(0.127440869853345,-0.107851473956683,
0.295024895857207));
#30423=CARTESIAN_POINT('Ctrl Pts',(0.120130224668095,-0.115939054735954,
0.294301803984655));
#30424=CARTESIAN_POINT('Ctrl Pts',(0.112109387908945,-0.123235729975854,
0.293578712112103));
#30425=CARTESIAN_POINT('Ctrl Pts',(0.103720296094471,-0.1308674123509,0.292822421429311));
#30426=CARTESIAN_POINT('Ctrl Pts',(0.0945548357077293,-0.137632876796364,
0.292066130746519));
#30427=CARTESIAN_POINT('Ctrl Pts',(0.084822406851203,-0.143390094832136,
0.291309840063728));
#30428=CARTESIAN_POINT('Ctrl Pts',(0.0750899779946767,-0.149147312867908,
0.290553549380936));
#30429=CARTESIAN_POINT('Ctrl Pts',(0.0647916243622132,-0.153895844390901,
0.289797258698145));
#30430=CARTESIAN_POINT('Ctrl Pts',(0.0541627183865265,-0.157549864922131,
0.289040968015353));
#30431=CARTESIAN_POINT('Ctrl Pts',(0.043977080418474,-0.16105149814234,
0.288316217687224));
#30432=CARTESIAN_POINT('Ctrl Pts',(0.0334129151605437,-0.163574190146975,
0.287591467359096));
#30433=CARTESIAN_POINT('Ctrl Pts',(0.0226796340738417,-0.165049066032731,
0.286866717030967));
#30434=CARTESIAN_POINT('Ctrl Pts',(0.0116431192534093,-0.166565609710283,
0.286121491253976));
#30435=CARTESIAN_POINT('Ctrl Pts',(0.000428707759892578,-0.16697376746695,
0.285376265476985));
#30436=CARTESIAN_POINT('Ctrl Pts',(-0.010722328474245,-0.166254598950196,
0.284631039699993));
#30437=CARTESIAN_POINT('Ctrl Pts',(-0.0215420873547145,-0.165556795644536,
0.28390795324872));
#30438=CARTESIAN_POINT('Ctrl Pts',(-0.0323012345614199,-0.163797936127461,
0.283184866797448));
#30439=CARTESIAN_POINT('Ctrl Pts',(-0.0427807792159435,-0.161013555111601,
0.282461780346175));
#30440=CARTESIAN_POINT('Ctrl Pts',(-0.0537416149776651,-0.158101296610015,
0.281705484906324));
#30441=CARTESIAN_POINT('Ctrl Pts',(-0.0643954292253115,-0.154067050397989,
0.280949189466473));
#30442=CARTESIAN_POINT('Ctrl Pts',(-0.0745093508587406,-0.14900978704303,
0.280192894026623));
#30443=CARTESIAN_POINT('Ctrl Pts',(-0.0846232724921697,-0.143952523688071,
0.279436598586772));
#30444=CARTESIAN_POINT('Ctrl Pts',(-0.0941963658250105,-0.137872881702097,
0.278680303146922));
#30445=CARTESIAN_POINT('Ctrl Pts',(-0.103028911236834,-0.130922127424483,
0.277924007707071));
#30446=CARTESIAN_POINT('Ctrl Pts',(-0.111391142551149,-0.124341485902893,
0.27720798337715));
#30447=CARTESIAN_POINT('Ctrl Pts',(-0.119154706145039,-0.116929141929537,
0.27649195904723));
#30448=CARTESIAN_POINT('Ctrl Pts',(-0.126150360403159,-0.108819329947179,
0.27577593471731));
#30449=CARTESIAN_POINT('Ctrl Pts',(-0.133136026511876,-0.100721096869485,
0.275060932701775));
#30450=CARTESIAN_POINT('Ctrl Pts',(-0.13935527853753,-0.0919280094024027,
0.27434593068624));
#30451=CARTESIAN_POINT('Ctrl Pts',(-0.144675018419886,-0.0826117367279351,
0.273630928670705));
#30452=CARTESIAN_POINT('Ctrl Pts',(-0.149989766192038,-0.0733042065598499,
0.272916597621972));
#30453=CARTESIAN_POINT('Ctrl Pts',(-0.154406198060711,-0.0634752687959111,
0.272202266573239));
#30454=CARTESIAN_POINT('Ctrl Pts',(-0.157835917236709,-0.0533233835202424,
0.271487935524506));
#30455=CARTESIAN_POINT('Ctrl Pts',(-0.161272582613367,-0.0431509376597016,
0.270772157743097));
#30456=CARTESIAN_POINT('Ctrl Pts',(-0.163718267329638,-0.032655136419677,
0.270056379961688));
#30457=CARTESIAN_POINT('Ctrl Pts',(-0.165134329484697,-0.022050243210436,
0.269340602180279));
#30458=CARTESIAN_POINT('Ctrl Pts',(-0.166116012306651,-0.0146984179710137,
0.26884439037924));
#30459=CARTESIAN_POINT('Ctrl Pts',(-0.166603948462927,-0.00729447879190147,
0.268348178578201));
#30460=CARTESIAN_POINT('Ctrl Pts',(-0.166599975890259,8.9629041933745E-5,
0.267851966777163));
#30461=CARTESIAN_POINT('Ctrl Pts',(-0.166813199754551,8.97901853038408E-5,
0.267851963660979));
#30462=CARTESIAN_POINT('Ctrl Pts',(-0.166846982879129,0.00527956240150659,
0.267503658240248));
#30463=CARTESIAN_POINT('Ctrl Pts',(-0.166013000560697,0.0248364214798825,
0.266190384413647));
#30464=CARTESIAN_POINT('Ctrl Pts',(-0.161420399274048,0.0440397124427515,
0.264877110587046));
#30465=CARTESIAN_POINT('Ctrl Pts',(-0.15630029400153,0.0575377421133763,
0.263912142181174));
#30466=CARTESIAN_POINT('',(-0.166599950277464,-0.000128714981079622,0.287148036339021));
#30467=CARTESIAN_POINT('Ctrl Pts',(-0.156342830333322,0.0575541432337077,
0.283376736141222));
#30468=CARTESIAN_POINT('Ctrl Pts',(-0.156693002305398,0.0566029193227644,
0.283444301107039));
#30469=CARTESIAN_POINT('Ctrl Pts',(-0.157034504006096,0.0556484700093607,
0.283511577341258));
#30470=CARTESIAN_POINT('Ctrl Pts',(-0.158330006516994,0.0519207991796621,
0.283772374119022));
#30471=CARTESIAN_POINT('Ctrl Pts',(-0.159219458012203,0.0491256176913406,
0.283963729442103));
#30472=CARTESIAN_POINT('Ctrl Pts',(-0.161652435568176,0.0407175964792538,
0.284528245306058));
#30473=CARTESIAN_POINT('Ctrl Pts',(-0.162976209044119,0.0350456580328451,
0.284894394953798));
#30474=CARTESIAN_POINT('Ctrl Pts',(-0.165738035686808,0.0195951430193326,
0.285867353567811));
#30475=CARTESIAN_POINT('Ctrl Pts',(-0.166607857439204,0.00974010186083236,
0.286461354741719));
#30476=CARTESIAN_POINT('Ctrl Pts',(-0.166599946525299,-0.000133483210403523,
0.287070783175954));
#30477=CARTESIAN_POINT('Ctrl Pts',(-0.166599950277464,-0.000128714981079622,
0.287148036339021));
#30478=CARTESIAN_POINT('Ctrl Pts',(-0.166593491893487,-0.00848800960612518,
0.287708823198405));
#30479=CARTESIAN_POINT('Ctrl Pts',(-0.165957778354428,-0.016823530277876,
0.288269610057788));
#30480=CARTESIAN_POINT('Ctrl Pts',(-0.16470404452251,-0.0250626757934412,
0.288830396917171));
#30481=CARTESIAN_POINT('Ctrl Pts',(-0.163083704256697,-0.0357110438081525,
0.289555164412204));
#30482=CARTESIAN_POINT('Ctrl Pts',(-0.16042046221447,-0.0462408744313591,
0.290279931907237));
#30483=CARTESIAN_POINT('Ctrl Pts',(-0.156750395020604,-0.056434684909944,
0.29100469940227));
#30484=CARTESIAN_POINT('Ctrl Pts',(-0.152976753205844,-0.0669161795098307,
0.291749920887535));
#30485=CARTESIAN_POINT('Ctrl Pts',(-0.148138610264182,-0.0770413696170685,
0.2924951423728));
#30486=CARTESIAN_POINT('Ctrl Pts',(-0.142331049133399,-0.0865877153676312,
0.293240363858066));
#30487=CARTESIAN_POINT('Ctrl Pts',(-0.136695862832195,-0.0958507150311191,
0.293963466346453));
#30488=CARTESIAN_POINT('Ctrl Pts',(-0.130148640486049,-0.104568014997532,
0.294686568834841));
#30489=CARTESIAN_POINT('Ctrl Pts',(-0.122822406993161,-0.112562055508978,
0.295409671323228));
#30490=CARTESIAN_POINT('Ctrl Pts',(-0.115160020039955,-0.120922890824665,
0.296165952306933));
#30491=CARTESIAN_POINT('Ctrl Pts',(-0.106645932747233,-0.128491508136188,
0.296922233290638));
#30492=CARTESIAN_POINT('Ctrl Pts',(-0.0974757874352491,-0.135107478933914,
0.297678514274342));
#30493=CARTESIAN_POINT('Ctrl Pts',(-0.0883056421232658,-0.141723449731641,
0.298434795258047));
#30494=CARTESIAN_POINT('Ctrl Pts',(-0.0784804380772645,-0.147386241101972,
0.299191076241752));
#30495=CARTESIAN_POINT('Ctrl Pts',(-0.068226779208863,-0.151989034468889,
0.299947357225456));
#30496=CARTESIAN_POINT('Ctrl Pts',(-0.0584000960596539,-0.156400161521043,
0.300672145683315));
#30497=CARTESIAN_POINT('Ctrl Pts',(-0.0481076509769673,-0.159870587002123,
0.301396934141173));
#30498=CARTESIAN_POINT('Ctrl Pts',(-0.0375517721827202,-0.16231273642551,
0.302121722599031));
#30499=CARTESIAN_POINT('Ctrl Pts',(-0.0266983814205212,-0.16482371656353,
0.30286693884359));
#30500=CARTESIAN_POINT('Ctrl Pts',(-0.015567356247688,-0.16624703322788,
0.303612155088149));
#30501=CARTESIAN_POINT('Ctrl Pts',(-0.00439723288282395,-0.166541959706778,
0.304357371332708));
#30502=CARTESIAN_POINT('Ctrl Pts',(0.00644176450877101,-0.166828143415863,
0.305080496464553));
#30503=CARTESIAN_POINT('Ctrl Pts',(0.0173166088560319,-0.166052040928164,
0.305803621596399));
#30504=CARTESIAN_POINT('Ctrl Pts',(0.0280059699158458,-0.164229186349664,
0.306526746728244));
#30505=CARTESIAN_POINT('Ctrl Pts',(0.0391851629624217,-0.162322800821581,
0.307283008529159));
#30506=CARTESIAN_POINT('Ctrl Pts',(0.0501603522143856,-0.159271323868591,
0.308039270330075));
#30507=CARTESIAN_POINT('Ctrl Pts',(0.060690698754633,-0.155152180405802,
0.30879553213099));
#30508=CARTESIAN_POINT('Ctrl Pts',(0.0712210452948805,-0.151033036943012,
0.309551793931906));
#30509=CARTESIAN_POINT('Ctrl Pts',(0.0813055599547078,-0.145846777599868,
0.310308055732821));
#30510=CARTESIAN_POINT('Ctrl Pts',(0.0907316620926344,-0.139725894142453,
0.311064317533737));
#30511=CARTESIAN_POINT('Ctrl Pts',(0.0997631054822526,-0.133861284186906,
0.311788915627706));
#30512=CARTESIAN_POINT('Ctrl Pts',(0.108256962643401,-0.127095724813711,
0.312513513721675));
#30513=CARTESIAN_POINT('Ctrl Pts',(0.116030006079989,-0.119551652807804,
0.313238111815644));
#30514=CARTESIAN_POINT('Ctrl Pts',(0.124024738902939,-0.111792421745177,
0.313983375651176));
#30515=CARTESIAN_POINT('Ctrl Pts',(0.131255976641635,-0.103210027724542,
0.314728639486707));
#30516=CARTESIAN_POINT('Ctrl Pts',(0.137560067724559,-0.0939829121043548,
0.315473903322238));
#30517=CARTESIAN_POINT('Ctrl Pts',(0.143675290244099,-0.0850322379328126,
0.316196839290341));
#30518=CARTESIAN_POINT('Ctrl Pts',(0.148917729715307,-0.075475816565885,
0.316919775258443));
#30519=CARTESIAN_POINT('Ctrl Pts',(0.153180499596328,-0.0655079731286148,
0.317642711226546));
#30520=CARTESIAN_POINT('Ctrl Pts',(0.157640752861041,-0.0550783446302099,
0.318399138995792));
#30521=CARTESIAN_POINT('Ctrl Pts',(0.16102766860715,-0.0441991294669704,
0.319155566765038));
#30522=CARTESIAN_POINT('Ctrl Pts',(0.163275721001094,-0.0331149351739208,
0.319911994534283));
#30523=CARTESIAN_POINT('Ctrl Pts',(0.165523773395038,-0.022030740880871,
0.320668422303529));
#30524=CARTESIAN_POINT('Ctrl Pts',(0.166632889218102,-0.01074270054802,
0.321424850072775));
#30525=CARTESIAN_POINT('Ctrl Pts',(0.166599254238088,0.000498485017781699,
0.322181277842021));
#30526=CARTESIAN_POINT('Ctrl Pts',(0.16656702045109,0.011271376245462,0.322906193735632));
#30527=CARTESIAN_POINT('Ctrl Pts',(0.165485420152532,0.0220807733691656,
0.323631109629243));
#30528=CARTESIAN_POINT('Ctrl Pts',(0.163358090325391,0.0327061817588259,
0.324356025522854));
#30529=CARTESIAN_POINT('Ctrl Pts',(0.161171280815181,0.0436286742749966,
0.325101209908475));
#30530=CARTESIAN_POINT('Ctrl Pts',(0.157879249630706,0.0543557147090324,
0.325846394294095));
#30531=CARTESIAN_POINT('Ctrl Pts',(0.15354319742141,0.0646532793105646,
0.326591578679716));
#30532=CARTESIAN_POINT('Ctrl Pts',(0.149334804488175,0.0746476696008179,
0.327314823823232));
#30533=CARTESIAN_POINT('Ctrl Pts',(0.144143535428062,0.0842366995458919,
0.328038068966747));
#30534=CARTESIAN_POINT('Ctrl Pts',(0.138074789796087,0.0932250632757434,
0.328761314110263));
#30535=CARTESIAN_POINT('Ctrl Pts',(0.131729906092074,0.102622412582131,
0.329517468116936));
#30536=CARTESIAN_POINT('Ctrl Pts',(0.124426154296712,0.111362075685159,
0.33027362212361));
#30537=CARTESIAN_POINT('Ctrl Pts',(0.116333209720592,0.119256632168214,
0.331029776130283));
#30538=CARTESIAN_POINT('Ctrl Pts',(0.108240265144473,0.127151188651269,
0.331785930136956));
#30539=CARTESIAN_POINT('Ctrl Pts',(0.0993590351697043,0.134199965056974,
0.33254208414363));
#30540=CARTESIAN_POINT('Ctrl Pts',(0.0898976910402409,0.14026391248512,
0.333298238150303));
#30541=CARTESIAN_POINT('Ctrl Pts',(0.0808267551962532,0.146077640146789,
0.334023190587172));
#30542=CARTESIAN_POINT('Ctrl Pts',(0.0711562522558495,0.151029111540782,
0.334748143024041));
#30543=CARTESIAN_POINT('Ctrl Pts',(0.0610735058921922,0.155001893143395,
0.33547309546091));
#30544=CARTESIAN_POINT('Ctrl Pts',(0.050709497637079,0.159085496939445,
0.336218270710716));
#30545=CARTESIAN_POINT('Ctrl Pts',(0.0399106851694592,0.162134323637613,
0.336963445960522));
#30546=CARTESIAN_POINT('Ctrl Pts',(0.0289069036702446,0.164073004849059,
0.337708621210329));
#30547=CARTESIAN_POINT('Ctrl Pts',(0.0182262189919821,0.165954761835291,
0.338431916367888));
#30548=CARTESIAN_POINT('Ctrl Pts',(0.00735340969149694,0.166790658058575,
0.339155211525448));
#30549=CARTESIAN_POINT('Ctrl Pts',(-0.0034902345256906,0.166563436152583,
0.339878506683008));
#30550=CARTESIAN_POINT('Ctrl Pts',(-0.0148259184032063,0.166325903857648,
0.340634621978938));
#30551=CARTESIAN_POINT('Ctrl Pts',(-0.0261286441049934,0.164926216810827,
0.341390737274867));
#30552=CARTESIAN_POINT('Ctrl Pts',(-0.0371490103249585,0.162405391018513,
0.342146852570797));
#30553=CARTESIAN_POINT('Ctrl Pts',(-0.0481693765449237,0.159884565226199,
0.342902967866727));
#30554=CARTESIAN_POINT('Ctrl Pts',(-0.0589063264950848,0.156242998178431,
0.343659083162657));
#30555=CARTESIAN_POINT('Ctrl Pts',(-0.0691302433640257,0.151580240969694,
0.344415198458586));
#30556=CARTESIAN_POINT('Ctrl Pts',(-0.079041259879042,0.147060186249601,
0.345148173039784));
#30557=CARTESIAN_POINT('Ctrl Pts',(-0.0885447161972927,0.141546778420546,
0.345881147620982));
#30558=CARTESIAN_POINT('Ctrl Pts',(-0.0974340198565392,0.135137603111035,
0.34661412220218));
#30559=CARTESIAN_POINT('Ctrl Pts',(-0.106194196036957,0.12882152853031,
0.347336449474731));
#30560=CARTESIAN_POINT('Ctrl Pts',(-0.114357173296284,0.121636065751674,
0.348058776747282));
#30561=CARTESIAN_POINT('Ctrl Pts',(-0.121751122610046,0.11371993731617,
0.348781104019834));
#30562=CARTESIAN_POINT('Ctrl Pts',(-0.12930855528541,0.105628779916766,
0.349519402255355));
#30563=CARTESIAN_POINT('Ctrl Pts',(-0.136061726017171,0.0967748355308142,
0.350257700490876));
#30564=CARTESIAN_POINT('Ctrl Pts',(-0.141866927035433,0.0873460646710723,
0.350995998726398));
#30565=CARTESIAN_POINT('Ctrl Pts',(-0.147672128053695,0.0779172938113303,
0.351734296961919));
#30566=CARTESIAN_POINT('Ctrl Pts',(-0.152528862308024,0.0679145886067279,
0.352472595197441));
#30567=CARTESIAN_POINT('Ctrl Pts',(-0.156342830367367,0.0575541431412265,
0.353210893432962));
#30568=CARTESIAN_POINT('Origin',(0.,0.,0.554592528053768));
#30569=CARTESIAN_POINT('',(-0.205640730232501,-0.000158877854750081,0.309592528053768));
#30570=CARTESIAN_POINT('Ctrl Pts',(0.125373879670659,0.163134317426071,
0.354786983357521));
#30571=CARTESIAN_POINT('Ctrl Pts',(0.174468778198734,0.124883730283729,
0.351399912090603));
#30572=CARTESIAN_POINT('Ctrl Pts',(0.23971402602582,-0.00512738462875954,
0.344307187387591));
#30573=CARTESIAN_POINT('Ctrl Pts',(0.13227703569284,-0.20370800021477,0.333508809248484));
#30574=CARTESIAN_POINT('Ctrl Pts',(-0.0994668003959092,-0.221581469162487,
0.322391848940201));
#30575=CARTESIAN_POINT('Ctrl Pts',(-0.200331019397092,-0.0888856881277869,
0.314419755208629));
#30576=CARTESIAN_POINT('Ctrl Pts',(-0.205728678103024,-0.0104771510256757,
0.310153314913151));
#30577=CARTESIAN_POINT('Ctrl Pts',(-0.205640730232501,-0.000158877854750081,
0.309592528053768));
#30578=CARTESIAN_POINT('Ctrl Pts',(-0.205640730232501,-0.000158877854750081,
0.309592528053768));
#30579=CARTESIAN_POINT('Ctrl Pts',(-0.205147522672671,0.0577055172922507,
0.306447661477057));
#30580=CARTESIAN_POINT('Ctrl Pts',(-0.149444666487041,0.184584641155565,
0.299597141464252));
#30581=CARTESIAN_POINT('Ctrl Pts',(0.0190813655878192,0.223159202921371,
0.291328296299053));
#30582=CARTESIAN_POINT('Ctrl Pts',(0.104339452755073,0.178824647059424,
0.286204317710565));
#30583=CARTESIAN_POINT('Ctrl Pts',(0.125045885691731,0.162713195961808,
0.284785992558171));
#30584=CARTESIAN_POINT('',(-0.205202343170581,0.000114209666698874,0.315407471946233));
#30585=CARTESIAN_POINT('Ctrl Pts',(-0.205202343170581,0.000114209666698874,
0.315407471946233));
#30586=CARTESIAN_POINT('Ctrl Pts',(-0.205338714105211,0.0268973406518496,
0.313959753808734));
#30587=CARTESIAN_POINT('Ctrl Pts',(-0.188013873562118,0.122066992862534,
0.308806382235141));
#30588=CARTESIAN_POINT('Ctrl Pts',(-0.0538860451750873,0.230976530846397,
0.300542700088359));
#30589=CARTESIAN_POINT('Ctrl Pts',(0.079577912064408,0.197485954337428,
0.293726736079075));
#30590=CARTESIAN_POINT('Ctrl Pts',(0.125296449978256,0.163038483752231,
0.290616425505885));
#30591=CARTESIAN_POINT('Ctrl Pts',(0.125005569899291,0.162656434463559,
0.360610754417505));
#30592=CARTESIAN_POINT('Ctrl Pts',(0.14989460202478,0.14362771524947,0.358917889200626));
#30593=CARTESIAN_POINT('Ctrl Pts',(0.215982794706034,0.0658033246759699,
0.353519370547653));
#30594=CARTESIAN_POINT('Ctrl Pts',(0.208602501412145,-0.124451281241526,
0.344415198458586));
#30595=CARTESIAN_POINT('Ctrl Pts',(0.00851095428263868,-0.242724098340208,
0.333298238150303));
#30596=CARTESIAN_POINT('Ctrl Pts',(-0.172282834993387,-0.152290880723065,
0.323628995979519));
#30597=CARTESIAN_POINT('Ctrl Pts',(-0.204989652081738,-0.0416581321254629,
0.317665407244829));
#30598=CARTESIAN_POINT('Ctrl Pts',(-0.205202343170581,0.000114209666698874,
0.315407471946233));
#30599=CARTESIAN_POINT('Ctrl Pts',(0.126643636228966,0.107786740449723,
0.399832185534737));
#30600=CARTESIAN_POINT('Ctrl Pts',(0.162509204878374,0.0656489274283753,
0.396125257297164));
#30601=CARTESIAN_POINT('Ctrl Pts',(0.188237171307053,-0.0564923230466638,
0.388712675623497));
#30602=CARTESIAN_POINT('Ctrl Pts',(0.0542929026994402,-0.189069324461983,
0.377594440513735));
#30603=CARTESIAN_POINT('Ctrl Pts',(-0.129318690295624,-0.147980389363182,
0.366477480205453));
#30604=CARTESIAN_POINT('Ctrl Pts',(-0.194518592522063,0.0283751522978791,
0.35536051989717));
#30605=CARTESIAN_POINT('Ctrl Pts',(-0.0815717939981551,0.178875911116407,
0.344243559588887));
#30606=CARTESIAN_POINT('Ctrl Pts',(0.106073156940092,0.165495539869897,
0.333126599280604));
#30607=CARTESIAN_POINT('Ctrl Pts',(0.196579733944809,0.000591879416301521,
0.322009638972321));
#30608=CARTESIAN_POINT('Ctrl Pts',(0.107059398326759,-0.164872578396621,
0.310892678664038));
#30609=CARTESIAN_POINT('Ctrl Pts',(-0.0805041914350236,-0.179338602839428,
0.299775718355756));
#30610=CARTESIAN_POINT('Ctrl Pts',(-0.194343207489227,-0.0295733312979194,
0.288658758047472));
#30611=CARTESIAN_POINT('Ctrl Pts',(-0.130204543087865,0.147277588040085,
0.277541797739191));
#30612=CARTESIAN_POINT('Ctrl Pts',(0.0531740072575756,0.189251798966039,
0.266424837430907));
#30613=CARTESIAN_POINT('Ctrl Pts',(0.187856398295355,0.0579119037769601,
0.255307877122625));
#30614=CARTESIAN_POINT('Ctrl Pts',(0.150501811766188,-0.126463503045677,
0.244190916814341));
#30615=CARTESIAN_POINT('Ctrl Pts',(-0.0246807683842457,-0.195024735134491,
0.233073956506059));
#30616=CARTESIAN_POINT('Ctrl Pts',(-0.177260962860889,-0.0849844321598874,
0.221956996197776));
#30617=CARTESIAN_POINT('Ctrl Pts',(-0.167507390899782,0.102883792677308,
0.210840035889493));
#30618=CARTESIAN_POINT('Ctrl Pts',(-0.00435228181763329,0.196532072723541,
0.199723075581211));
#30619=CARTESIAN_POINT('Ctrl Pts',(0.162788607054259,0.110198321346856,
0.188606115272927));
#30620=CARTESIAN_POINT('Ctrl Pts',(0.180849360257203,-0.0770539217729518,
0.177489154964645));
#30621=CARTESIAN_POINT('Ctrl Pts',(0.0332901492326799,-0.193740978540385,
0.166372194656362));
#30622=CARTESIAN_POINT('Ctrl Pts',(-0.144755865067518,-0.133002038301909,
0.155255234348079));
#30623=CARTESIAN_POINT('Ctrl Pts',(-0.190235897869724,0.0495387808087312,
0.144138274039796));
#30624=CARTESIAN_POINT('Ctrl Pts',(-0.0614999585747447,0.186712527814268,
0.133021313731514));
#30625=CARTESIAN_POINT('Ctrl Pts',(0.123557201881564,0.152896804553835,
0.121904353423231));
#30626=CARTESIAN_POINT('Ctrl Pts',(0.195461582000762,-0.0209401151255174,
0.110787393114948));
#30627=CARTESIAN_POINT('Ctrl Pts',(0.0883649656983379,-0.175600523395451,
0.0996704328066651));
#30628=CARTESIAN_POINT('Ctrl Pts',(-0.099656720083647,-0.16944734392556,
0.0885534724983826));
#30629=CARTESIAN_POINT('Ctrl Pts',(-0.19641124121612,-0.00811687322483667,
0.0774365121900994));
#30630=CARTESIAN_POINT('Ctrl Pts',(-0.11329927613454,0.160648547782502,
0.0663195518818169));
#30631=CARTESIAN_POINT('Ctrl Pts',(0.0735803580016403,0.182290627941773,
0.0552025915735339));
#30632=CARTESIAN_POINT('Ctrl Pts',(0.193057988403518,0.0369986682686435,
0.0440856312652511));
#30633=CARTESIAN_POINT('Ctrl Pts',(0.135769225220844,-0.142187434876412,
0.0329686709569682));
#30634=CARTESIAN_POINT('Ctrl Pts',(-0.0459207683190805,-0.191138471118919,
0.0218517106486855));
#30635=CARTESIAN_POINT('Ctrl Pts',(-0.185432287088896,-0.0650875272293826,
0.0107347503404028));
#30636=CARTESIAN_POINT('Ctrl Pts',(-0.155367407483271,0.120647823966984,
-0.000382209967880125));
#30637=CARTESIAN_POINT('Ctrl Pts',(0.0174625308446545,0.195743738997455,
-0.0114991702761629));
#30638=CARTESIAN_POINT('Ctrl Pts',(0.12128809756269,0.126513168479806,-0.0189104771483514));
#30639=CARTESIAN_POINT('Ctrl Pts',(0.147094871950923,0.0775866671285812,
-0.0226161305844457));
#30640=CARTESIAN_POINT('Ctrl Pts',(0.136651966898638,0.116304857682842,
0.407420004843589));
#30641=CARTESIAN_POINT('Ctrl Pts',(0.175351901974875,0.0708369984075165,
0.403713076606016));
#30642=CARTESIAN_POINT('Ctrl Pts',(0.203113085414244,-0.0609567704218693,
0.396300494932349));
#30643=CARTESIAN_POINT('Ctrl Pts',(0.058583535370867,-0.204011001557275,
0.385182259822589));
#30644=CARTESIAN_POINT('Ctrl Pts',(-0.139538423815494,-0.15967491041038,
0.374065299514305));
#30645=CARTESIAN_POINT('Ctrl Pts',(-0.20989091167942,0.030617569804638,
0.362948339206022));
#30646=CARTESIAN_POINT('Ctrl Pts',(-0.0880182094041043,0.193012028181579,
0.35183137889774));
#30647=CARTESIAN_POINT('Ctrl Pts',(0.114455853942829,0.178574239571626,
0.340714418589457));
#30648=CARTESIAN_POINT('Ctrl Pts',(0.212114939967467,0.000638654170180345,
0.329597458281175));
#30649=CARTESIAN_POINT('Ctrl Pts',(0.115520035526191,-0.17790204700704,
0.318480497972891));
#30650=CARTESIAN_POINT('Ctrl Pts',(-0.0868662368734497,-0.193511285277326,
0.307363537664609));
#30651=CARTESIAN_POINT('Ctrl Pts',(-0.209701666404921,-0.0319104379022986,
0.296246577356326));
#30652=CARTESIAN_POINT('Ctrl Pts',(-0.140494283344222,0.158916568451797,
0.285129617048043));
#30653=CARTESIAN_POINT('Ctrl Pts',(0.0573762164132184,0.204207896566219,
0.27401265673976));
#30654=CARTESIAN_POINT('Ctrl Pts',(0.202702220861237,0.0624885370762606,
0.262895696431478));
#30655=CARTESIAN_POINT('Ctrl Pts',(0.162395594536428,-0.1364575982392,0.251778736123194));
#30656=CARTESIAN_POINT('Ctrl Pts',(-0.0266312279456287,-0.21043705347998,
0.240661775814911));
#30657=CARTESIAN_POINT('Ctrl Pts',(-0.191269454593774,-0.0917005398472298,
0.229544815506629));
#30658=CARTESIAN_POINT('Ctrl Pts',(-0.180745082170017,0.111014442177949,
0.218427855198346));
#30659=CARTESIAN_POINT('Ctrl Pts',(-0.00469623179329347,0.21206351219877,
0.207310894890063));
#30660=CARTESIAN_POINT('Ctrl Pts',(0.175653384607776,0.118907019802798,
0.196193934581781));
#30661=CARTESIAN_POINT('Ctrl Pts',(0.195141434085374,-0.0831433010063813,
0.185076974273498));
#30662=CARTESIAN_POINT('Ctrl Pts',(0.035920986687165,-0.209051844804459,
0.173960013965215));
#30663=CARTESIAN_POINT('Ctrl Pts',(-0.156195560002925,-0.143512857626925,
0.162843053656931));
#30664=CARTESIAN_POINT('Ctrl Pts',(-0.205269766351514,0.0534537070858774,
0.151726093348649));
#30665=CARTESIAN_POINT('Ctrl Pts',(-0.0663601468946243,0.201467953149315,
0.140609133040367));
#30666=CARTESIAN_POINT('Ctrl Pts',(0.133321619343601,0.164979857629981,
0.129492172732083));
#30667=CARTESIAN_POINT('Ctrl Pts',(0.210908423264415,-0.0225949601905965,
0.118375212423801));
#30668=CARTESIAN_POINT('Ctrl Pts',(0.0953482285187782,-0.189477794739203,
0.107258252115518));
#30669=CARTESIAN_POINT('Ctrl Pts',(-0.107532342086862,-0.182838344844378,
0.0961412918072349));
#30670=CARTESIAN_POINT('Ctrl Pts',(-0.211933131678721,-0.00875832946896322,
0.0850243314989519));
#30671=CARTESIAN_POINT('Ctrl Pts',(-0.122253035312291,0.173344201789962,
0.0739073711906692));
#30672=CARTESIAN_POINT('Ctrl Pts',(0.0793952301547247,0.196696601559939,
0.0627904108823863));
#30673=CARTESIAN_POINT('Ctrl Pts',(0.208314879660736,0.0399225807319636,
0.0516734505741035));
#30674=CARTESIAN_POINT('Ctrl Pts',(0.146498728425558,-0.153424153180541,
0.0405564902658207));
#30675=CARTESIAN_POINT('Ctrl Pts',(-0.0495497720939863,-0.206243667713202,
0.0294395299575379));
#30676=CARTESIAN_POINT('Ctrl Pts',(-0.200086538192865,-0.0702312321511612,
0.0183225696492552));
#30677=CARTESIAN_POINT('Ctrl Pts',(-0.167645706146228,0.130182320549621,
0.00720560934097224));
#30678=CARTESIAN_POINT('Ctrl Pts',(0.0188425510985476,0.211212878424741,
-0.00391135096731048));
#30679=CARTESIAN_POINT('Ctrl Pts',(0.130873193370489,0.136511188608702,
-0.011322657839499));
#30680=CARTESIAN_POINT('Ctrl Pts',(0.158719412765877,0.0837181478985793,
-0.0150283112755933));
#30681=CARTESIAN_POINT('Ctrl Pts',(0.146660297568308,0.124822974915961,
0.415007824152442));
#30682=CARTESIAN_POINT('Ctrl Pts',(0.188194599071376,0.0760250693866577,
0.411300895914869));
#30683=CARTESIAN_POINT('Ctrl Pts',(0.217988999521435,-0.065421217797075,
0.403888314241202));
#30684=CARTESIAN_POINT('Ctrl Pts',(0.0628741680422935,-0.218952678652567,
0.39277007913144));
#30685=CARTESIAN_POINT('Ctrl Pts',(-0.149758157335363,-0.171369431457579,
0.381653118823158));
#30686=CARTESIAN_POINT('Ctrl Pts',(-0.225263230836776,0.0328599873113971,
0.370536158514874));
#30687=CARTESIAN_POINT('Ctrl Pts',(-0.0944646248100532,0.207148145246751,
0.359419198206592));
#30688=CARTESIAN_POINT('Ctrl Pts',(0.122838550945567,0.191652939273356,
0.348302237898309));
#30689=CARTESIAN_POINT('Ctrl Pts',(0.227650145990125,0.000685428924058993,
0.337185277590026));
#30690=CARTESIAN_POINT('Ctrl Pts',(0.123980672725625,-0.190931515617459,
0.326068317281743));
#30691=CARTESIAN_POINT('Ctrl Pts',(-0.093228282311876,-0.207683967715224,
0.314951356973461));
#30692=CARTESIAN_POINT('Ctrl Pts',(-0.225060125320616,-0.0342475445066776,
0.303834396665177));
#30693=CARTESIAN_POINT('Ctrl Pts',(-0.15078402360058,0.170555548863508,
0.292717436356895));
#30694=CARTESIAN_POINT('Ctrl Pts',(0.0615784255688618,0.219163994166401,
0.281600476048612));
#30695=CARTESIAN_POINT('Ctrl Pts',(0.217548043427119,0.0670651703755612,
0.27048351574033));
#30696=CARTESIAN_POINT('Ctrl Pts',(0.174289377306668,-0.146451693432721,
0.259366555432046));
#30697=CARTESIAN_POINT('Ctrl Pts',(-0.0285816875070117,-0.225849371825467,
0.248249595123764));
#30698=CARTESIAN_POINT('Ctrl Pts',(-0.205277946326661,-0.0984166475345728,
0.237132634815481));
#30699=CARTESIAN_POINT('Ctrl Pts',(-0.193982773440251,0.11914509167859,
0.226015674507198));
#30700=CARTESIAN_POINT('Ctrl Pts',(-0.00504018176895369,0.227594951673999,
0.214898714198915));
#30701=CARTESIAN_POINT('Ctrl Pts',(0.188518162161292,0.127615718258739,
0.203781753890632));
#30702=CARTESIAN_POINT('Ctrl Pts',(0.209433507913547,-0.0892326802398108,
0.19266479358235));
#30703=CARTESIAN_POINT('Ctrl Pts',(0.0385518241416503,-0.224362711068533,
0.181547833274067));
#30704=CARTESIAN_POINT('Ctrl Pts',(-0.167635254938332,-0.154023676951941,
0.170430872965784));
#30705=CARTESIAN_POINT('Ctrl Pts',(-0.220303634833304,0.0573686333630237,
0.159313912657501));
#30706=CARTESIAN_POINT('Ctrl Pts',(-0.0712203352145041,0.216223378484361,
0.148196952349218));
#30707=CARTESIAN_POINT('Ctrl Pts',(0.143086036805638,0.177062910706128,
0.137079992040936));
#30708=CARTESIAN_POINT('Ctrl Pts',(0.226355264528068,-0.0242498052556755,
0.125963031732653));
#30709=CARTESIAN_POINT('Ctrl Pts',(0.102331491339218,-0.203355066082957,
0.11484607142437));
#30710=CARTESIAN_POINT('Ctrl Pts',(-0.115407964090077,-0.196229345763195,
0.103729111116087));
#30711=CARTESIAN_POINT('Ctrl Pts',(-0.227455022141321,-0.00939978571308979,
0.0926121508078043));
#30712=CARTESIAN_POINT('Ctrl Pts',(-0.131206794490042,0.186039855797424,
0.0814951904995215));
#30713=CARTESIAN_POINT('Ctrl Pts',(0.0852101023078094,0.211102575178107,
0.0703782301912387));
#30714=CARTESIAN_POINT('Ctrl Pts',(0.223571770917953,0.0428464931952837,
0.0592612698829559));
#30715=CARTESIAN_POINT('Ctrl Pts',(0.157228231630271,-0.164660871484669,
0.048144309574673));
#30716=CARTESIAN_POINT('Ctrl Pts',(-0.0531787758688922,-0.221348864307486,
0.0370273492663903));
#30717=CARTESIAN_POINT('Ctrl Pts',(-0.214740789296835,-0.0753749370729399,
0.0259103889581075));
#30718=CARTESIAN_POINT('Ctrl Pts',(-0.179924004809185,0.139716817132259,
0.0147934286498247));
#30719=CARTESIAN_POINT('Ctrl Pts',(0.0202225713524407,0.226682017852026,
0.00367646834154192));
#30720=CARTESIAN_POINT('Ctrl Pts',(0.140458289178288,0.146509208737597,
-0.0037348385306466));
#30721=CARTESIAN_POINT('Ctrl Pts',(0.17034395358083,0.0898496286685773,
-0.00744049196674088));
#30722=CARTESIAN_POINT('Ctrl Pts',(0.15666862823798,0.133341092149081,0.422595643461294));
#30723=CARTESIAN_POINT('Ctrl Pts',(0.201037296167877,0.0812131403657989,
0.418888715223721));
#30724=CARTESIAN_POINT('Ctrl Pts',(0.232864913628626,-0.0698856651722803,
0.411476133550053));
#30725=CARTESIAN_POINT('Ctrl Pts',(0.0671648007137202,-0.233894355747859,
0.400357898440292));
#30726=CARTESIAN_POINT('Ctrl Pts',(-0.159977890855233,-0.183063952504777,
0.38924093813201));
#30727=CARTESIAN_POINT('Ctrl Pts',(-0.240635549994133,0.0351024048181559,
0.378123977823728));
#30728=CARTESIAN_POINT('Ctrl Pts',(-0.100911040216002,0.221284262311923,
0.367007017515444));
#30729=CARTESIAN_POINT('Ctrl Pts',(0.131221247948303,0.204731638975084,
0.355890057207162));
#30730=CARTESIAN_POINT('Ctrl Pts',(0.243185352012785,0.000732203677937851,
0.344773096898879));
#30731=CARTESIAN_POINT('Ctrl Pts',(0.132441309925057,-0.203960984227879,
0.333656136590596));
#30732=CARTESIAN_POINT('Ctrl Pts',(-0.0995903277503024,-0.221856650153122,
0.322539176282312));
#30733=CARTESIAN_POINT('Ctrl Pts',(-0.240418584236309,-0.0365846511110568,
0.311422215974029));
#30734=CARTESIAN_POINT('Ctrl Pts',(-0.161073763856939,0.182194529275218,
0.300305255665748));
#30735=CARTESIAN_POINT('Ctrl Pts',(0.0657806347245049,0.234120091766581,
0.289188295357465));
#30736=CARTESIAN_POINT('Ctrl Pts',(0.232393865993,0.0716418036748616,0.278071335049182));
#30737=CARTESIAN_POINT('Ctrl Pts',(0.186183160076907,-0.156445788626244,
0.2669543747409));
#30738=CARTESIAN_POINT('Ctrl Pts',(-0.0305321470683947,-0.241261690170956,
0.255837414432615));
#30739=CARTESIAN_POINT('Ctrl Pts',(-0.219286438059546,-0.105132755221915,
0.244720454124334));
#30740=CARTESIAN_POINT('Ctrl Pts',(-0.207220464710484,0.127275741179231,
0.233603493816051));
#30741=CARTESIAN_POINT('Ctrl Pts',(-0.00538413174461367,0.243126391149227,
0.222486533507768));
#30742=CARTESIAN_POINT('Ctrl Pts',(0.201382939714809,0.136324416714681,
0.211369573199485));
#30743=CARTESIAN_POINT('Ctrl Pts',(0.223725581741719,-0.0953220594732403,
0.200252612891201));
#30744=CARTESIAN_POINT('Ctrl Pts',(0.0411826615961353,-0.239673577332608,
0.18913565258292));
#30745=CARTESIAN_POINT('Ctrl Pts',(-0.179074949873739,-0.164534496276958,
0.178018692274637));
#30746=CARTESIAN_POINT('Ctrl Pts',(-0.235337503315095,0.06128355964017,
0.166901731966353));
#30747=CARTESIAN_POINT('Ctrl Pts',(-0.0760805235343836,0.230978803819408,
0.155784771658071));
#30748=CARTESIAN_POINT('Ctrl Pts',(0.152850454267675,0.189145963782275,
0.144667811349788));
#30749=CARTESIAN_POINT('Ctrl Pts',(0.241802105791721,-0.0259046503207544,
0.133550851041506));
#30750=CARTESIAN_POINT('Ctrl Pts',(0.109314754159658,-0.217232337426711,
0.122433890733223));
#30751=CARTESIAN_POINT('Ctrl Pts',(-0.123283586093291,-0.209620346682013,
0.11131693042494));
#30752=CARTESIAN_POINT('Ctrl Pts',(-0.242976912603923,-0.0100412419572166,
0.100199970116657));
#30753=CARTESIAN_POINT('Ctrl Pts',(-0.140160553667793,0.198735509804885,
0.0890830098083741));
#30754=CARTESIAN_POINT('Ctrl Pts',(0.091024974460894,0.225508548796274,
0.0779660495000909));
#30755=CARTESIAN_POINT('Ctrl Pts',(0.23882866217517,0.0457704056586039,
0.0668490891918084));
#30756=CARTESIAN_POINT('Ctrl Pts',(0.167957734834984,-0.175897589788799,
0.0557321288835253));
#30757=CARTESIAN_POINT('Ctrl Pts',(-0.0568077796437977,-0.236454060901771,
0.0446151685752427));
#30758=CARTESIAN_POINT('Ctrl Pts',(-0.229395040400805,-0.0805186419947185,
0.0334982082669599));
#30759=CARTESIAN_POINT('Ctrl Pts',(-0.192202303472141,0.149251313714896,
0.0223812479586771));
#30760=CARTESIAN_POINT('Ctrl Pts',(0.0216025916063335,0.242151157279311,
0.0112642876503943));
#30761=CARTESIAN_POINT('Ctrl Pts',(0.150043384986088,0.156507228866493,
0.00385298077820578));
#30762=CARTESIAN_POINT('Ctrl Pts',(0.181968494395784,0.0959811094385754,
0.000147327342111498));
#30763=CARTESIAN_POINT('Ctrl Pts',(0.181742788875947,0.0958620587959227,
0.));
#30764=CARTESIAN_POINT('Ctrl Pts',(0.174504469275331,0.106933967990604,
-2.81788574158242E-17));
#30765=CARTESIAN_POINT('Ctrl Pts',(0.16615526098928,0.117183932420547,-9.27869193614022E-17));
#30766=CARTESIAN_POINT('Ctrl Pts',(0.156880171409737,0.126533297037827,
2.04697370165263E-16));
#30767=CARTESIAN_POINT('Ctrl Pts',(0.15128023158171,0.13217808125668,3.25645692820429E-16));
#30768=CARTESIAN_POINT('Ctrl Pts',(0.145341937935802,0.13749388649769,2.01225074043376E-16));
#30769=CARTESIAN_POINT('Ctrl Pts',(0.139101245907215,0.142455889753469,
1.66533453693773E-16));
#30770=CARTESIAN_POINT('Ctrl Pts',(0.135040637805532,0.145684498139958,
1.43960784828397E-16));
#30771=CARTESIAN_POINT('Ctrl Pts',(0.130850103351038,0.148764420786474,
-1.1266670458931E-16));
#30772=CARTESIAN_POINT('Ctrl Pts',(0.126545459943985,0.151683176533579,
-1.52655665885959E-16));
#30773=CARTESIAN_POINT('Ctrl Pts',(0.122352033792771,0.154526521619693,
-1.91611449258523E-16));
#30774=CARTESIAN_POINT('Ctrl Pts',(0.118059533786955,0.157210759147407,
9.00868310955262E-17));
#30775=CARTESIAN_POINT('Ctrl Pts',(0.113682253713289,0.159728355552366,
6.59194920871187E-17));
#30776=CARTESIAN_POINT('Ctrl Pts',(0.10257577466787,0.166116256542462,4.59966795815047E-18));
#30777=CARTESIAN_POINT('Ctrl Pts',(0.0909137787356949,0.171441652247163,
8.12077434941466E-17));
#30778=CARTESIAN_POINT('Ctrl Pts',(0.0788520591185822,0.175593194714427,
2.0643209364124E-16));
#30779=CARTESIAN_POINT('Ctrl Pts',(0.0732665345230194,0.177515685312495,
2.64420814148192E-16));
#30780=CARTESIAN_POINT('Ctrl Pts',(0.0675951556350182,0.179185757356502,
3.458479309827E-16));
#30781=CARTESIAN_POINT('Ctrl Pts',(0.0618535813722568,0.180588437047447,
4.28476698566271E-16));
#30782=CARTESIAN_POINT('Ctrl Pts',(0.0574839813535566,0.181655940300613,
4.91360961288444E-16));
#30783=CARTESIAN_POINT('Ctrl Pts',(0.0530766090871315,0.182567386168162,
3.40638383294036E-16));
#30784=CARTESIAN_POINT('Ctrl Pts',(0.0486558084301484,0.183314182850192,
3.10515502199848E-16));
#30785=CARTESIAN_POINT('Ctrl Pts',(0.0379659386233148,0.18512000037568,
2.37675828554995E-16));
#30786=CARTESIAN_POINT('Ctrl Pts',(0.0271690281402411,0.185972684584687,
4.74617282448999E-16));
#30787=CARTESIAN_POINT('Ctrl Pts',(0.0163641619208266,0.185791435560747,
4.23272528138341E-16));
#30788=CARTESIAN_POINT('Ctrl Pts',(0.00736772073510989,0.185640522430428,
4.3031952015864E-16));
#30789=CARTESIAN_POINT('Ctrl Pts',(-0.00163453813579219,0.184771897471073,
6.67878087952716E-16));
#30790=CARTESIAN_POINT('Ctrl Pts',(-0.0105685044149961,0.183215538395939,
5.27355936696949E-16));
#30791=CARTESIAN_POINT('Ctrl Pts',(-0.0151046453702256,0.182425311085791,
3.9707342353691E-16));
#30792=CARTESIAN_POINT('Ctrl Pts',(-0.0196162098916884,0.181458430012929,
3.63725539130059E-16));
#30793=CARTESIAN_POINT('Ctrl Pts',(-0.024079466750711,0.180323824810446,
3.90312782094782E-16));
#30794=CARTESIAN_POINT('Ctrl Pts',(-0.0350902229812683,0.177524778800534,
4.55902924086132E-16));
#30795=CARTESIAN_POINT('Ctrl Pts',(-0.0458352633172663,0.173702776386141,
3.51897032873533E-16));
#30796=CARTESIAN_POINT('Ctrl Pts',(-0.0561677502272309,0.168929888351253,
4.75314232417645E-16));
#30797=CARTESIAN_POINT('Ctrl Pts',(-0.0622728678478303,0.166109749976353,
5.48237288230581E-16));
#30798=CARTESIAN_POINT('Ctrl Pts',(-0.0682334189441441,0.162957096799898,
5.45378188703878E-16));
#30799=CARTESIAN_POINT('Ctrl Pts',(-0.0740150970940476,0.159481877940378,
3.75567632548979E-16));
#30800=CARTESIAN_POINT('Ctrl Pts',(-0.0784470916501901,0.156817919368583,
2.45397906573034E-16));
#30801=CARTESIAN_POINT('Ctrl Pts',(-0.0827700074415804,0.153966080728667,
4.80659032402892E-16));
#30802=CARTESIAN_POINT('Ctrl Pts',(-0.0869532130138509,0.15094253677905,
4.90059381963448E-16));
#30803=CARTESIAN_POINT('Ctrl Pts',(-0.0932798978419366,0.146369725497697,
5.0427648124676E-16));
#30804=CARTESIAN_POINT('Ctrl Pts',(-0.0992975790462204,0.141398564153525,
4.93000331800633E-16));
#30805=CARTESIAN_POINT('Ctrl Pts',(-0.104950075896856,0.136047484562577,
5.88938620094126E-16));
#30806=CARTESIAN_POINT('Ctrl Pts',(-0.109220306833978,0.132004962077368,
6.61416085814314E-16));
#30807=CARTESIAN_POINT('Ctrl Pts',(-0.113281874229585,0.12774440154114,
3.167752875038E-16));
#30808=CARTESIAN_POINT('Ctrl Pts',(-0.117092856033647,0.123291942798165,
3.49980461278321E-16));
#30809=CARTESIAN_POINT('Ctrl Pts',(-0.12264309442135,0.116807470107011,
3.98339818428034E-16));
#30810=CARTESIAN_POINT('Ctrl Pts',(-0.127672471608383,0.109907592598991,
9.25668074629998E-17));
#30811=CARTESIAN_POINT('Ctrl Pts',(-0.132096989238305,0.102614780608902,
6.74915852372227E-17));
#30812=CARTESIAN_POINT('Ctrl Pts',(-0.13264315472071,0.101714550908896,
7.80582634118999E-17));
#30813=CARTESIAN_POINT('Ctrl Pts',(-0.133180081100841,0.100808327459116,
-1.29750824392398E-16));
#30814=CARTESIAN_POINT('Ctrl Pts',(-0.13370774202371,0.0998962637199363,
8.4296718910748E-17));
#30815=CARTESIAN_POINT('Ctrl Pts',(0.126907087985239,0.10793586530485,0.4));
#30816=CARTESIAN_POINT('Ctrl Pts',(0.135120918952714,0.100273232772193,
0.4));
#30817=CARTESIAN_POINT('Ctrl Pts',(0.142440334671478,0.0917705069751104,
0.4));
#30818=CARTESIAN_POINT('Ctrl Pts',(0.148860643047527,0.08262174487072,0.4));
#30819=CARTESIAN_POINT('Ctrl Pts',(0.153627635655852,0.0758289120700936,
0.4));
#30820=CARTESIAN_POINT('Ctrl Pts',(0.157898622412177,0.0686786359713564,
0.4));
#30821=CARTESIAN_POINT('Ctrl Pts',(0.161661540307137,0.0612359751064182,
0.4));
#30822=CARTESIAN_POINT('Ctrl Pts',(0.164102874102171,0.056407270361387,
0.4));
#30823=CARTESIAN_POINT('Ctrl Pts',(0.166331409569869,0.0514502806578965,
0.4));
#30824=CARTESIAN_POINT('Ctrl Pts',(0.168329235075816,0.0464171379264235,
0.4));
#30825=CARTESIAN_POINT('Ctrl Pts',(0.172801737816196,0.0351495149071816,
0.4));
#30826=CARTESIAN_POINT('Ctrl Pts',(0.176138845697143,0.0234718063959593,
0.4));
#30827=CARTESIAN_POINT('Ctrl Pts',(0.17831042601693,0.0115813652209228,
0.4));
#30828=CARTESIAN_POINT('Ctrl Pts',(0.179431215733824,0.00544450531438937,
0.4));
#30829=CARTESIAN_POINT('Ctrl Pts',(0.180240887278069,-0.000749624549012006,
0.4));
#30830=CARTESIAN_POINT('Ctrl Pts',(0.180730523800757,-0.00697642912666059,
0.4));
#30831=CARTESIAN_POINT('Ctrl Pts',(0.181117091707021,-0.0118924897078438,
0.4));
#30832=CARTESIAN_POINT('Ctrl Pts',(0.181303371987996,-0.0168290189998756,
0.4));
#30833=CARTESIAN_POINT('Ctrl Pts',(0.181285629855571,-0.021746975072603,
0.4));
#30834=CARTESIAN_POINT('Ctrl Pts',(0.181246813532722,-0.0325065030763667,
0.4));
#30835=CARTESIAN_POINT('Ctrl Pts',(0.180236611938718,-0.0432078221541177,
0.4));
#30836=CARTESIAN_POINT('Ctrl Pts',(0.178223999863926,-0.0537244994070257,
0.4));
#30837=CARTESIAN_POINT('Ctrl Pts',(0.177057515641798,-0.059819831060048,
0.4));
#30838=CARTESIAN_POINT('Ctrl Pts',(0.175553812784225,-0.0658533566784224,
0.4));
#30839=CARTESIAN_POINT('Ctrl Pts',(0.173731861666494,-0.071808724503393,
0.4));
#30840=CARTESIAN_POINT('Ctrl Pts',(0.171731410043636,-0.0783475526389198,
0.4));
#30841=CARTESIAN_POINT('Ctrl Pts',(0.169342367274103,-0.084801264593441,
0.4));
#30842=CARTESIAN_POINT('Ctrl Pts',(0.166610322749882,-0.0910962279747303,
0.4));
#30843=CARTESIAN_POINT('Ctrl Pts',(0.161428849033874,-0.103034974585266,
0.4));
#30844=CARTESIAN_POINT('Ctrl Pts',(0.155012393449103,-0.114432718842341,
0.4));
#30845=CARTESIAN_POINT('Ctrl Pts',(0.147536507995649,-0.125146591163663,
0.4));
#30846=CARTESIAN_POINT('Ctrl Pts',(0.143512554735272,-0.130913415940082,
0.4));
#30847=CARTESIAN_POINT('Ctrl Pts',(0.139180426978968,-0.136482273587012,
0.4));
#30848=CARTESIAN_POINT('Ctrl Pts',(0.13456102284103,-0.141828718973796,
0.4));
#30849=CARTESIAN_POINT('Ctrl Pts',(0.131202022825332,-0.145716387080307,
0.4));
#30850=CARTESIAN_POINT('Ctrl Pts',(0.127692523532622,-0.149483993751978,
0.4));
#30851=CARTESIAN_POINT('Ctrl Pts',(0.124053969377856,-0.15310949025686,
0.4));
#30852=CARTESIAN_POINT('Ctrl Pts',(0.117250830652081,-0.159888214613682,
0.4));
#30853=CARTESIAN_POINT('Ctrl Pts',(0.109987812654579,-0.16618218257803,
0.399999999999999));
#30854=CARTESIAN_POINT('Ctrl Pts',(0.102320566390068,-0.171932690825377,
0.399999999999999));
#30855=CARTESIAN_POINT('Ctrl Pts',(0.0968356651066751,-0.176046419402484,
0.4));
#30856=CARTESIAN_POINT('Ctrl Pts',(0.0911417236297836,-0.179882091250733,
0.4));
#30857=CARTESIAN_POINT('Ctrl Pts',(0.0852821558629418,-0.183402277546523,
0.4));
#30858=CARTESIAN_POINT('Ctrl Pts',(0.0761595778105699,-0.1888827456493,
0.4));
#30859=CARTESIAN_POINT('Ctrl Pts',(0.0666264887468849,-0.193608063008219,
0.4));
#30860=CARTESIAN_POINT('Ctrl Pts',(0.0567496916571122,-0.197494094154161,
0.4));
#30861=CARTESIAN_POINT('Ctrl Pts',(0.0555606243966102,-0.197961933309601,
0.4));
#30862=CARTESIAN_POINT('Ctrl Pts',(0.0543665677551527,-0.198417583105329,
0.4));
#30863=CARTESIAN_POINT('Ctrl Pts',(0.0531676903274471,-0.198861095112417,
0.4));
#30864=CARTESIAN_POINT('Ctrl Pts',(-0.0530701539231891,-0.198716381290575,
0.39988111122049));
#30865=CARTESIAN_POINT('Ctrl Pts',(-0.119166933292682,-0.181064257030941,
0.396175457784396));
#30866=CARTESIAN_POINT('Ctrl Pts',(-0.231217597730413,-0.0749271919797139,
0.388764150912208));
#30867=CARTESIAN_POINT('Ctrl Pts',(-0.188233160600942,0.154135205755113,
0.377647190603924));
#30868=CARTESIAN_POINT('Ctrl Pts',(0.027448085609834,0.241502672443478,
0.366530230295642));
#30869=CARTESIAN_POINT('Ctrl Pts',(0.217832547874475,0.107973703950356,
0.355413269987359));
#30870=CARTESIAN_POINT('Ctrl Pts',(0.2088115571148,-0.124576002900519,0.344296309679076));
#30871=CARTESIAN_POINT('Ctrl Pts',(0.00851948372747169,-0.242967349770974,
0.333179349370793));
#30872=CARTESIAN_POINT('Ctrl Pts',(-0.199551799190759,-0.138889905056905,
0.322062389062511));
#30873=CARTESIAN_POINT('Ctrl Pts',(-0.224887572854444,0.0924014979391681,
0.310945428754227));
#30874=CARTESIAN_POINT('Ctrl Pts',(-0.044267354029904,0.239062074042455,
0.299828468445945));
#30875=CARTESIAN_POINT('Ctrl Pts',(0.17688916429529,0.166797563884364,0.288711508137662));
#30876=CARTESIAN_POINT('Ctrl Pts',(0.236054132464953,-0.0582213149159194,
0.277594547829379));
#30877=CARTESIAN_POINT('Ctrl Pts',(0.0790422580723326,-0.229920204906449,
0.266477587521096));
#30878=CARTESIAN_POINT('Ctrl Pts',(-0.1503552283045,-0.191061333140319,
0.255360627212814));
#30879=CARTESIAN_POINT('Ctrl Pts',(-0.242059194800053,0.0227699515372025,
0.24424366690453));
#30880=CARTESIAN_POINT('Ctrl Pts',(-0.112087717542688,0.215748532186423,
0.233126706596248));
#30881=CARTESIAN_POINT('Ctrl Pts',(0.12053246817559,0.211146946028599,0.222009746287965));
#30882=CARTESIAN_POINT('Ctrl Pts',(0.2427702968486,0.0131791041947362,0.210892785979682));
#30883=CARTESIAN_POINT('Ctrl Pts',(0.142681575266364,-0.196857993321032,
0.199775825671399));
#30884=CARTESIAN_POINT('Ctrl Pts',(-0.088073456719532,-0.226614588589072,
0.188658865363117));
#30885=CARTESIAN_POINT('Ctrl Pts',(-0.238171720883513,-0.0488398692285348,
0.177541905054834));
#30886=CARTESIAN_POINT('Ctrl Pts',(-0.170154794877542,0.17366188873646,
0.166424944746551));
#30887=CARTESIAN_POINT('Ctrl Pts',(0.0536881709643731,0.237125892724105,
0.155307984438268));
#30888=CARTESIAN_POINT('Ctrl Pts',(0.22836399769663,0.0834324284708191,
0.144191024129985));
#30889=CARTESIAN_POINT('Ctrl Pts',(0.193906557049213,-0.146667554740565,
0.133074063821703));
#30890=CARTESIAN_POINT('Ctrl Pts',(-0.0181287510056,-0.242450976667101,
0.12195710351342));
#30891=CARTESIAN_POINT('Ctrl Pts',(-0.213561473377095,-0.116200156085957,
0.110840143205137));
#30892=CARTESIAN_POINT('Ctrl Pts',(-0.213417683574561,0.116465305142727,
0.0997231828968541));
#30893=CARTESIAN_POINT('Ctrl Pts',(-0.0178264954593966,0.242473544582663,
0.0886062225885714));
#30894=CARTESIAN_POINT('Ctrl Pts',(0.194086798383876,0.146426051546118,
0.0774892622802885));
#30895=CARTESIAN_POINT('Ctrl Pts',(0.228263539268917,-0.08371507562078,
0.0663723019720058));
#30896=CARTESIAN_POINT('Ctrl Pts',(0.053387176172982,-0.23719429948306,
0.0552553416637228));
#30897=CARTESIAN_POINT('Ctrl Pts',(-0.170358267049339,-0.173446751211026,
0.0441383813554401));
#30898=CARTESIAN_POINT('Ctrl Pts',(-0.238134013450897,0.0491287952340117,
0.0330214210471573));
#30899=CARTESIAN_POINT('Ctrl Pts',(-0.0877476633139311,0.226737044263148,
0.0219044607388744));
#30900=CARTESIAN_POINT('Ctrl Pts',(0.142841392439922,0.196655218102167,
0.0107875004305917));
#30901=CARTESIAN_POINT('Ctrl Pts',(0.242917667120415,-0.0134309867011242,
-0.00032945987769134));
#30902=CARTESIAN_POINT('Ctrl Pts',(0.11992182972462,-0.211425239089247,
-0.0114476947911144));
#30903=CARTESIAN_POINT('Ctrl Pts',(-0.03443369593138,-0.214017241553922,
-0.0188602762684437));
#30904=CARTESIAN_POINT('Ctrl Pts',(-0.0951131155041543,-0.182368133997801,
-0.0225672043096786));
#30905=CARTESIAN_POINT('Ctrl Pts',(-0.0496833462568047,-0.18603478695103,
0.407459442196852));
#30906=CARTESIAN_POINT('Ctrl Pts',(-0.111561990525051,-0.169509178168571,
0.403753788760758));
#30907=CARTESIAN_POINT('Ctrl Pts',(-0.216461855100954,-0.0701455215028423,
0.396342481888569));
#30908=CARTESIAN_POINT('Ctrl Pts',(-0.176220579813749,0.144298673204884,
0.385225521580286));
#30909=CARTESIAN_POINT('Ctrl Pts',(0.0256964157935848,0.22609056145417,
0.374108561272003));
#30910=CARTESIAN_POINT('Ctrl Pts',(0.203931006450699,0.101083085753992,
0.362991600963721));
#30911=CARTESIAN_POINT('Ctrl Pts',(0.195485713298902,-0.116625866515355,
0.351874640655438));
#30912=CARTESIAN_POINT('Ctrl Pts',(0.00797579107409027,-0.227461766650253,
0.340757680347155));
#30913=CARTESIAN_POINT('Ctrl Pts',(-0.18681689052028,-0.130026290379794,
0.329640720038872));
#30914=CARTESIAN_POINT('Ctrl Pts',(-0.210535796959459,0.0865046599149425,
0.318523759730589));
#30915=CARTESIAN_POINT('Ctrl Pts',(-0.04144231956296,0.223805716085013,
0.307406799422307));
#30916=CARTESIAN_POINT('Ctrl Pts',(0.165600529658904,0.156152950550184,
0.296289839114023));
#30917=CARTESIAN_POINT('Ctrl Pts',(0.22098973399588,-0.0545057727302003,
0.285172878805742));
#30918=CARTESIAN_POINT('Ctrl Pts',(0.0739979741232949,-0.215247258719768,
0.274055918497458));
#30919=CARTESIAN_POINT('Ctrl Pts',(-0.140759924687336,-0.178868265285912,
0.262938958189176));
#30920=CARTESIAN_POINT('Ctrl Pts',(-0.226611567912552,0.0213168288170191,
0.251821997880892));
#30921=CARTESIAN_POINT('Ctrl Pts',(-0.104934553042155,0.201979987556277,
0.24070503757261));
#30922=CARTESIAN_POINT('Ctrl Pts',(0.112840380305332,0.197672063393468,
0.229588077264327));
#30923=CARTESIAN_POINT('Ctrl Pts',(0.227277289164333,0.0123380459383872,
0.218471116956044));
#30924=CARTESIAN_POINT('Ctrl Pts',(0.133575985452863,-0.184294996764932,
0.207354156647761));
#30925=CARTESIAN_POINT('Ctrl Pts',(-0.082452823720155,-0.212152598765963,
0.196237196339479));
#30926=CARTESIAN_POINT('Ctrl Pts',(-0.22297218309111,-0.0457230280042223,
0.185120236031196));
#30927=CARTESIAN_POINT('Ctrl Pts',(-0.159295931257184,0.162579210947684,
0.174003275722913));
#30928=CARTESIAN_POINT('Ctrl Pts',(0.0502619229591482,0.221993097131716,
0.16288631541463));
#30929=CARTESIAN_POINT('Ctrl Pts',(0.213790364855006,0.0781079745644107,
0.151769355106347));
#30930=CARTESIAN_POINT('Ctrl Pts',(0.181531913950816,-0.137307589447754,
0.140652394798065));
#30931=CARTESIAN_POINT('Ctrl Pts',(-0.0169718183730586,-0.226978347217279,
0.129535434489782));
#30932=CARTESIAN_POINT('Ctrl Pts',(-0.199932501501024,-0.108784545797044,
0.118418474181499));
#30933=CARTESIAN_POINT('Ctrl Pts',(-0.199797888012663,0.109032773688304,
0.107301513873216));
#30934=CARTESIAN_POINT('Ctrl Pts',(-0.0166888520379352,0.226999474903564,
0.0961845535649328));
#30935=CARTESIAN_POINT('Ctrl Pts',(0.181700652723512,0.137081498397608,
0.0850675932566501));
#30936=CARTESIAN_POINT('Ctrl Pts',(0.213696317438905,-0.0783725838632703,
0.0739506329483673));
#30937=CARTESIAN_POINT('Ctrl Pts',(0.0499801369205431,-0.222057138338313,
0.0628336726400844));
#30938=CARTESIAN_POINT('Ctrl Pts',(-0.159486418331701,-0.16237780297392,
0.0517167123318017));
#30939=CARTESIAN_POINT('Ctrl Pts',(-0.222936882054789,0.0459935154573673,
0.0405997520235189));
#30940=CARTESIAN_POINT('Ctrl Pts',(-0.0821478216543599,0.212267239617864,
0.029482791715236));
#30941=CARTESIAN_POINT('Ctrl Pts',(0.133725603484557,0.184105162165512,
0.0183658314069533));
#30942=CARTESIAN_POINT('Ctrl Pts',(0.227415254625167,-0.012573853918123,
0.00724887109867029));
#30943=CARTESIAN_POINT('Ctrl Pts',(0.112268711309588,-0.197932596470366,
-0.00386936381475281));
#30944=CARTESIAN_POINT('Ctrl Pts',(-0.0322362215179624,-0.200359183665446,
-0.0112819452920821));
#30945=CARTESIAN_POINT('Ctrl Pts',(-0.0890432286666411,-0.170729844890482,
-0.0149888733333169));
#30946=CARTESIAN_POINT('Ctrl Pts',(-0.0462965385904204,-0.173353192611486,
0.415037773173213));
#30947=CARTESIAN_POINT('Ctrl Pts',(-0.103957047757422,-0.1579540993062,
0.411332119737119));
#30948=CARTESIAN_POINT('Ctrl Pts',(-0.201706112471495,-0.0653638510259706,
0.40392081286493));
#30949=CARTESIAN_POINT('Ctrl Pts',(-0.164207999026558,0.134462140654653,
0.392803852556647));
#30950=CARTESIAN_POINT('Ctrl Pts',(0.0239447459773354,0.210678450464861,
0.381686892248365));
#30951=CARTESIAN_POINT('Ctrl Pts',(0.190029465026925,0.0941924675576273,
0.370569931940081));
#30952=CARTESIAN_POINT('Ctrl Pts',(0.182159869483005,-0.108675730130192,
0.359452971631799));
#30953=CARTESIAN_POINT('Ctrl Pts',(0.00743209842070957,-0.211956183529533,
0.348336011323516));
#30954=CARTESIAN_POINT('Ctrl Pts',(-0.174081981849801,-0.121162675702683,
0.337219051015233));
#30955=CARTESIAN_POINT('Ctrl Pts',(-0.196184021064473,0.0806078218907167,
0.326102090706951));
#30956=CARTESIAN_POINT('Ctrl Pts',(-0.0386172850960161,0.208549358127571,
0.314985130398667));
#30957=CARTESIAN_POINT('Ctrl Pts',(0.15431189502252,0.145508337216003,0.303868170090385));
#30958=CARTESIAN_POINT('Ctrl Pts',(0.205925335526805,-0.0507902305444811,
0.292751209782102));
#30959=CARTESIAN_POINT('Ctrl Pts',(0.0689536901742569,-0.200574312533087,
0.281634249473819));
#30960=CARTESIAN_POINT('Ctrl Pts',(-0.131164621070171,-0.166675197431506,
0.270517289165536));
#30961=CARTESIAN_POINT('Ctrl Pts',(-0.211163941025053,0.0198637060968362,
0.259400328857254));
#30962=CARTESIAN_POINT('Ctrl Pts',(-0.0977813885416242,0.188211442926131,
0.248283368548971));
#30963=CARTESIAN_POINT('Ctrl Pts',(0.105148292435073,0.184197180758337,
0.237166408240688));
#30964=CARTESIAN_POINT('Ctrl Pts',(0.211784281480065,0.0114969876820384,
0.226049447932405));
#30965=CARTESIAN_POINT('Ctrl Pts',(0.124470395639363,-0.171732000208833,
0.214932487624122));
#30966=CARTESIAN_POINT('Ctrl Pts',(-0.0768321907207784,-0.197690608942853,
0.20381552731584));
#30967=CARTESIAN_POINT('Ctrl Pts',(-0.207772645298705,-0.0426061867799098,
0.192698567007556));
#30968=CARTESIAN_POINT('Ctrl Pts',(-0.148437067636826,0.151496533158908,
0.181581606699274));
#30969=CARTESIAN_POINT('Ctrl Pts',(0.0468356749539237,0.206860301539328,
0.170464646390991));
#30970=CARTESIAN_POINT('Ctrl Pts',(0.199216732013379,0.0727835206580018,
0.159347686082708));
#30971=CARTESIAN_POINT('Ctrl Pts',(0.169157270852419,-0.127947624154943,
0.148230725774426));
#30972=CARTESIAN_POINT('Ctrl Pts',(-0.0158148857405171,-0.211505717767457,
0.137113765466142));
#30973=CARTESIAN_POINT('Ctrl Pts',(-0.186303529624954,-0.101368935508133,
0.12599680515786));
#30974=CARTESIAN_POINT('Ctrl Pts',(-0.186178092450765,0.101600242233881,
0.114879844849577));
#30975=CARTESIAN_POINT('Ctrl Pts',(-0.015551208616474,0.211525405224465,
0.103762884541294));
#30976=CARTESIAN_POINT('Ctrl Pts',(0.16931450706315,0.1277369452491,0.0926459242330117));
#30977=CARTESIAN_POINT('Ctrl Pts',(0.199129095608893,-0.0730300921057608,
0.0815289639247289));
#30978=CARTESIAN_POINT('Ctrl Pts',(0.0465730976681044,-0.206919977193565,
0.0704120036164461));
#30979=CARTESIAN_POINT('Ctrl Pts',(-0.148614569614064,-0.151308854736816,
0.0592950433081632));
#30980=CARTESIAN_POINT('Ctrl Pts',(-0.207739750658681,0.0428582356807231,
0.0481780829998806));
#30981=CARTESIAN_POINT('Ctrl Pts',(-0.0765479799947886,0.197797434972579,
0.0370611226915976));
#30982=CARTESIAN_POINT('Ctrl Pts',(0.124609814529192,0.171555106228858,
0.025944162383315));
#30983=CARTESIAN_POINT('Ctrl Pts',(0.211912842129918,-0.0117167211351222,
0.0148272020750319));
#30984=CARTESIAN_POINT('Ctrl Pts',(0.104615592894555,-0.184439953851485,
0.00370896716160887));
#30985=CARTESIAN_POINT('Ctrl Pts',(-0.0300387471045446,-0.186701125776971,
-0.00370361431572043));
#30986=CARTESIAN_POINT('Ctrl Pts',(-0.0829733418291278,-0.159091555783164,
-0.00741054235695528));
#30987=CARTESIAN_POINT('Ctrl Pts',(-0.0429097309240361,-0.160671598271941,
0.422616104149575));
#30988=CARTESIAN_POINT('Ctrl Pts',(-0.0963521049897916,-0.14639902044383,
0.41891045071348));
#30989=CARTESIAN_POINT('Ctrl Pts',(-0.186950369842037,-0.0605821805490989,
0.411499143841292));
#30990=CARTESIAN_POINT('Ctrl Pts',(-0.152195418239366,0.124625608104424,
0.400382183533009));
#30991=CARTESIAN_POINT('Ctrl Pts',(0.022193076161086,0.195266339475553,
0.389265223224726));
#30992=CARTESIAN_POINT('Ctrl Pts',(0.17612792360315,0.0873018493612629,
0.378148262916443));
#30993=CARTESIAN_POINT('Ctrl Pts',(0.168834025667108,-0.100725593745027,
0.367031302608161));
#30994=CARTESIAN_POINT('Ctrl Pts',(0.00688840576732832,-0.196450600408813,
0.355914342299878));
#30995=CARTESIAN_POINT('Ctrl Pts',(-0.161347073179323,-0.112299061025572,
0.344797381991595));
#30996=CARTESIAN_POINT('Ctrl Pts',(-0.181832245169488,0.074710983866491,
0.333680421683312));
#30997=CARTESIAN_POINT('Ctrl Pts',(-0.0357922506290721,0.193293000170129,
0.322563461375029));
#30998=CARTESIAN_POINT('Ctrl Pts',(0.143023260386134,0.134863723881822,
0.311446501066746));
#30999=CARTESIAN_POINT('Ctrl Pts',(0.190860937057732,-0.0470746883587621,
0.300329540758464));
#31000=CARTESIAN_POINT('Ctrl Pts',(0.0639094062252192,-0.185901366346407,
0.28921258045018));
#31001=CARTESIAN_POINT('Ctrl Pts',(-0.121569317453007,-0.154482129577099,
0.278095620141899));
#31002=CARTESIAN_POINT('Ctrl Pts',(-0.195716314137552,0.0184105833766533,
0.266978659833615));
#31003=CARTESIAN_POINT('Ctrl Pts',(-0.090628224041093,0.174442898295985,
0.255861699525333));
#31004=CARTESIAN_POINT('Ctrl Pts',(0.0974562045648148,0.170722298123207,
0.244744739217049));
#31005=CARTESIAN_POINT('Ctrl Pts',(0.196291273795798,0.0106559294256891,
0.233627778908767));
#31006=CARTESIAN_POINT('Ctrl Pts',(0.115364805825862,-0.159169003652733,
0.222510818600484));
#31007=CARTESIAN_POINT('Ctrl Pts',(-0.0712115577214017,-0.183228619119744,
0.211393858292202));
#31008=CARTESIAN_POINT('Ctrl Pts',(-0.192573107506301,-0.0394893455555971,
0.200276897983918));
#31009=CARTESIAN_POINT('Ctrl Pts',(-0.137578204016468,0.140413855370133,
0.189159937675636));
#31010=CARTESIAN_POINT('Ctrl Pts',(0.0434094269486991,0.191727505946939,
0.178042977367353));
#31011=CARTESIAN_POINT('Ctrl Pts',(0.184643099171754,0.0674590667515935,
0.16692601705907));
#31012=CARTESIAN_POINT('Ctrl Pts',(0.156782627754022,-0.118587658862133,
0.155809056750787));
#31013=CARTESIAN_POINT('Ctrl Pts',(-0.0146579531079754,-0.196033088317636,
0.144692096442504));
#31014=CARTESIAN_POINT('Ctrl Pts',(-0.172674557748884,-0.09395332521922,
0.133575136134222));
#31015=CARTESIAN_POINT('Ctrl Pts',(-0.172558296888866,0.0941677107794582,
0.122458175825939));
#31016=CARTESIAN_POINT('Ctrl Pts',(-0.014413565195013,0.196051335545365,
0.111341215517656));
#31017=CARTESIAN_POINT('Ctrl Pts',(0.156928361402787,0.118392392100591,
0.100224255209373));
#31018=CARTESIAN_POINT('Ctrl Pts',(0.18456187377888,-0.0676876003482512,
0.0891072949010907));
#31019=CARTESIAN_POINT('Ctrl Pts',(0.043166058415666,-0.191782816048817,
0.0779903345928075));
#31020=CARTESIAN_POINT('Ctrl Pts',(-0.137742720896427,-0.140239906499711,
0.0668733742845249));
#31021=CARTESIAN_POINT('Ctrl Pts',(-0.192542619262574,0.0397229559040788,
0.0557564139762422));
#31022=CARTESIAN_POINT('Ctrl Pts',(-0.0709481383352174,0.183327630327294,
0.0446394536679593));
#31023=CARTESIAN_POINT('Ctrl Pts',(0.115494025573827,0.159005050292203,
0.0335224933596767));
#31024=CARTESIAN_POINT('Ctrl Pts',(0.19641042963467,-0.0108595883521212,
0.0224055330513936));
#31025=CARTESIAN_POINT('Ctrl Pts',(0.0969624744795222,-0.170947311232604,
0.0112872981379705));
#31026=CARTESIAN_POINT('Ctrl Pts',(-0.027841272691127,-0.173043067888495,
0.00387471666064119));
#31027=CARTESIAN_POINT('Ctrl Pts',(-0.0769034549916146,-0.147453266675846,
0.000167788619406336));
#31028=CARTESIAN_POINT('Ctrl Pts',(-0.0769902040670465,-0.147743251885541,
-6.93889390390723E-18));
#31029=CARTESIAN_POINT('Ctrl Pts',(-0.0676919232959199,-0.154046060402415,
-2.05855969193849E-16));
#31030=CARTESIAN_POINT('Ctrl Pts',(-0.0577736401978069,-0.159289942753595,
-1.00246838828094E-16));
#31031=CARTESIAN_POINT('Ctrl Pts',(-0.0474255897416162,-0.163513503779695,
-1.90819582357449E-16));
#31032=CARTESIAN_POINT('Ctrl Pts',(-0.0397423269308822,-0.166649430638389,
-3.11176017719216E-16));
#31033=CARTESIAN_POINT('Ctrl Pts',(-0.0318209566269663,-0.169222252729945,
1.95009950297112E-17));
#31034=CARTESIAN_POINT('Ctrl Pts',(-0.0237275895516037,-0.171234685365662,
-2.0122792321331E-16));
#31035=CARTESIAN_POINT('Ctrl Pts',(-0.0184767120920151,-0.172540327018564,
-2.79520754060125E-16));
#31036=CARTESIAN_POINT('Ctrl Pts',(-0.0131481186698344,-0.173609960486947,
-2.33518219162689E-16));
#31037=CARTESIAN_POINT('Ctrl Pts',(-0.00779661953491697,-0.174437723369069,
-1.66533453693773E-16));
#31038=CARTESIAN_POINT('Ctrl Pts',(0.00418371951149402,-0.176290826532845,
-1.65754361308467E-17));
#31039=CARTESIAN_POINT('Ctrl Pts',(0.0163112126214376,-0.176945748924033,
2.86527215930858E-16));
#31040=CARTESIAN_POINT('Ctrl Pts',(0.0283867514614758,-0.176417025598077,
4.31946145518225E-16));
#31041=CARTESIAN_POINT('Ctrl Pts',(0.0346191147784547,-0.17614414370807,
5.06998995280064E-16));
#31042=CARTESIAN_POINT('Ctrl Pts',(0.0408380822565802,-0.17555520239787,
4.4015761051379E-16));
#31043=CARTESIAN_POINT('Ctrl Pts',(0.0470176916982643,-0.174646980992462,
2.72351585728359E-16));
#31044=CARTESIAN_POINT('Ctrl Pts',(0.0518965299270048,-0.173929934817509,
1.39867735986388E-16));
#31045=CARTESIAN_POINT('Ctrl Pts',(0.0567507558014769,-0.173013065902084,
2.5227236170911E-16));
#31046=CARTESIAN_POINT('Ctrl Pts',(0.0615414748941956,-0.171901420573325,
2.04697370165263E-16));
#31047=CARTESIAN_POINT('Ctrl Pts',(0.0720225956837857,-0.169469366274084,
1.00612947078832E-16));
#31048=CARTESIAN_POINT('Ctrl Pts',(0.0822308156893155,-0.166103230285251,
6.54325850411354E-17));
#31049=CARTESIAN_POINT('Ctrl Pts',(0.0920359693799996,-0.161800897340594,
4.85722573273506E-17));
#31050=CARTESIAN_POINT('Ctrl Pts',(0.097718907582874,-0.159307321714552,
2.35558750287395E-17));
#31051=CARTESIAN_POINT('Ctrl Pts',(0.103266552483572,-0.156498733846988,
1.93700674136354E-16));
#31052=CARTESIAN_POINT('Ctrl Pts',(0.108667183415534,-0.15339726738813,
3.00107161343988E-16));
#31053=CARTESIAN_POINT('Ctrl Pts',(0.11459693992244,-0.149991935465425,
-9.62025511039274E-17));
#31054=CARTESIAN_POINT('Ctrl Pts',(0.120357245189988,-0.146226692136978,
-9.37471224547374E-17));
#31055=CARTESIAN_POINT('Ctrl Pts',(0.125886456988692,-0.142162369288104,
-1.00613961606655E-16));
#31056=CARTESIAN_POINT('Ctrl Pts',(0.136372892719963,-0.134454171104081,
-1.13637276694791E-16));
#31057=CARTESIAN_POINT('Ctrl Pts',(0.146057084193878,-0.125662334494057,
2.63201407223155E-16));
#31058=CARTESIAN_POINT('Ctrl Pts',(0.154838806086005,-0.115989804239992,
1.60461921527855E-16));
#31059=CARTESIAN_POINT('Ctrl Pts',(0.159565621700614,-0.110783505566531,
1.05161763860969E-16));
#31060=CARTESIAN_POINT('Ctrl Pts',(0.164030860393261,-0.105320811841541,
2.34445481277501E-16));
#31061=CARTESIAN_POINT('Ctrl Pts',(0.168215340079027,-0.0996275370064118,
1.8995222061946E-16));
#31062=CARTESIAN_POINT('Ctrl Pts',(0.171258070102838,-0.0954876917746175,
1.57599099030174E-16));
#31063=CARTESIAN_POINT('Ctrl Pts',(0.174150262314154,-0.0912278383229185,
-1.38974090381786E-17));
#31064=CARTESIAN_POINT('Ctrl Pts',(0.176875192571848,-0.0868737897286597,
-2.68882138776405E-17));
#31065=CARTESIAN_POINT('Ctrl Pts',(0.18196979446539,-0.0787333449777348,
-5.11761672103458E-17));
#31066=CARTESIAN_POINT('Ctrl Pts',(0.186489538005871,-0.0702524649460043,
-1.10733251100512E-16));
#31067=CARTESIAN_POINT('Ctrl Pts',(0.190389583958077,-0.0614984559805871,
1.94289029309402E-16));
#31068=CARTESIAN_POINT('Ctrl Pts',(0.193180561397451,-0.0552338524795093,
4.12571150485138E-16));
#31069=CARTESIAN_POINT('Ctrl Pts',(0.19565375183857,-0.0488272373071404,
6.43798831786931E-17));
#31070=CARTESIAN_POINT('Ctrl Pts',(0.197782303704477,-0.0423293043071611,
-3.20923843055709E-17));
#31071=CARTESIAN_POINT('Ctrl Pts',(0.201094791365034,-0.0322171133728858,
-1.82224124455317E-16));
#31072=CARTESIAN_POINT('Ctrl Pts',(0.203579910696782,-0.0218728104555898,
-6.96994360509918E-17));
#31073=CARTESIAN_POINT('Ctrl Pts',(0.205170522984607,-0.0113802171361648,
-1.25713241899694E-16));
#31074=CARTESIAN_POINT('Ctrl Pts',(0.205362040344674,-0.0101168584986283,
-9.17536921087371E-17));
#31075=CARTESIAN_POINT('Ctrl Pts',(0.205540563699428,-0.00885134802550821,
-3.06470418352831E-16));
#31076=CARTESIAN_POINT('Ctrl Pts',(0.205706180843763,-0.00758383860674098,
-1.47153339860595E-16));
#31077=CARTESIAN_POINT('Ctrl Pts',(-0.0530170217188623,-0.198517432567172,
0.4));
#31078=CARTESIAN_POINT('Ctrl Pts',(-0.0654220238787413,-0.193924320176368,
0.4));
#31079=CARTESIAN_POINT('Ctrl Pts',(-0.07727288556064,-0.188065277790972,
0.4));
#31080=CARTESIAN_POINT('Ctrl Pts',(-0.0884517548081647,-0.181103168839149,
0.4));
#31081=CARTESIAN_POINT('Ctrl Pts',(-0.0952010467673211,-0.17689976463727,
0.4));
#31082=CARTESIAN_POINT('Ctrl Pts',(-0.101704904097436,-0.172293295443026,
0.4));
#31083=CARTESIAN_POINT('Ctrl Pts',(-0.107931126215051,-0.167313289922026,
0.4));
#31084=CARTESIAN_POINT('Ctrl Pts',(-0.111959846876041,-0.164090942444648,
0.4));
#31085=CARTESIAN_POINT('Ctrl Pts',(-0.11587376397307,-0.160710653528623,
0.4));
#31086=CARTESIAN_POINT('Ctrl Pts',(-0.119657579752374,-0.157184731207288,
0.4));
#31087=CARTESIAN_POINT('Ctrl Pts',(-0.123317881187486,-0.153773904865407,
0.4));
#31088=CARTESIAN_POINT('Ctrl Pts',(-0.126848621970303,-0.150234155769173,
0.4));
#31089=CARTESIAN_POINT('Ctrl Pts',(-0.130239379311871,-0.146577572125245,
0.4));
#31090=CARTESIAN_POINT('Ctrl Pts',(-0.138953512703323,-0.137180273993772,
0.4));
#31091=CARTESIAN_POINT('Ctrl Pts',(-0.146755875032497,-0.127003654809211,
0.4));
#31092=CARTESIAN_POINT('Ctrl Pts',(-0.153503490990357,-0.116175026119951,
0.4));
#31093=CARTESIAN_POINT('Ctrl Pts',(-0.156641420012712,-0.111139252233509,
0.4));
#31094=CARTESIAN_POINT('Ctrl Pts',(-0.159550584997633,-0.105962198003635,
0.4));
#31095=CARTESIAN_POINT('Ctrl Pts',(-0.162212724451348,-0.100655900626943,
0.4));
#31096=CARTESIAN_POINT('Ctrl Pts',(-0.164244214036353,-0.0966066432371229,
0.4));
#31097=CARTESIAN_POINT('Ctrl Pts',(-0.166130198465154,-0.0924843279899854,
0.4));
#31098=CARTESIAN_POINT('Ctrl Pts',(-0.16785638026916,-0.0883115908809607,
0.4));
#31099=CARTESIAN_POINT('Ctrl Pts',(-0.172012349337959,-0.0782652757610305,
0.4));
#31100=CARTESIAN_POINT('Ctrl Pts',(-0.175258071106289,-0.0679005050150562,
0.4));
#31101=CARTESIAN_POINT('Ctrl Pts',(-0.177491918105115,-0.0572965665658759,
0.4));
#31102=CARTESIAN_POINT('Ctrl Pts',(-0.179346683049967,-0.0484921080137729,
0.4));
#31103=CARTESIAN_POINT('Ctrl Pts',(-0.180503025417514,-0.039522267403315,
0.4));
#31104=CARTESIAN_POINT('Ctrl Pts',(-0.180973680426715,-0.0304659686020515,
0.4));
#31105=CARTESIAN_POINT('Ctrl Pts',(-0.181212650830767,-0.0258677228776098,
0.4));
#31106=CARTESIAN_POINT('Ctrl Pts',(-0.181273928531148,-0.0212541273507348,
0.4));
#31107=CARTESIAN_POINT('Ctrl Pts',(-0.181160938580718,-0.0166503054466016,
0.4));
#31108=CARTESIAN_POINT('Ctrl Pts',(-0.180882194042426,-0.00529274483024155,
0.4));
#31109=CARTESIAN_POINT('Ctrl Pts',(-0.179547011733344,0.00603339551763739,
0.4));
#31110=CARTESIAN_POINT('Ctrl Pts',(-0.177192981605961,0.0171689196549591,
0.4));
#31111=CARTESIAN_POINT('Ctrl Pts',(-0.175802060433226,0.0237485450012686,
0.4));
#31112=CARTESIAN_POINT('Ctrl Pts',(-0.174054789653161,0.0302612200901589,
0.4));
#31113=CARTESIAN_POINT('Ctrl Pts',(-0.171953235151015,0.0366712838759848,
0.4));
#31114=CARTESIAN_POINT('Ctrl Pts',(-0.170342278092587,0.0415849501597783,
0.4));
#31115=CARTESIAN_POINT('Ctrl Pts',(-0.168523879724122,0.0464340797721413,
0.4));
#31116=CARTESIAN_POINT('Ctrl Pts',(-0.166506993102895,0.0511852100193018,
0.4));
#31117=CARTESIAN_POINT('Ctrl Pts',(-0.163456650544741,0.0583708270191453,
0.4));
#31118=CARTESIAN_POINT('Ctrl Pts',(-0.159949186498915,0.0653438287379616,
0.4));
#31119=CARTESIAN_POINT('Ctrl Pts',(-0.155990069415437,0.0720453408263799,
0.4));
#31120=CARTESIAN_POINT('Ctrl Pts',(-0.152999118912724,0.0771080582270448,
0.4));
#31121=CARTESIAN_POINT('Ctrl Pts',(-0.149749165779154,0.0820158613244291,
0.4));
#31122=CARTESIAN_POINT('Ctrl Pts',(-0.146256365994585,0.0867220621721572,
0.4));
#31123=CARTESIAN_POINT('Ctrl Pts',(-0.141169509830996,0.0935760956885117,
0.4));
#31124=CARTESIAN_POINT('Ctrl Pts',(-0.135561760713222,0.100014759881837,
0.4));
#31125=CARTESIAN_POINT('Ctrl Pts',(-0.129436334451722,0.105951160758884,
0.4));
#31126=CARTESIAN_POINT('Ctrl Pts',(-0.128680208499678,0.106683953314577,
0.4));
#31127=CARTESIAN_POINT('Ctrl Pts',(-0.127916183191217,0.107409072087309,
0.4));
#31128=CARTESIAN_POINT('Ctrl Pts',(-0.127144402274346,0.108126457236474,
0.4));
#31129=CARTESIAN_POINT('Origin',(0.,0.,0.4));
#31130=CARTESIAN_POINT('',(0.202072594216369,-0.35,0.4));
#31131=CARTESIAN_POINT('',(0.404145188432738,0.,0.4));
#31132=CARTESIAN_POINT('',(0.202072594216369,-0.35,0.4));
#31133=CARTESIAN_POINT('',(0.202072594216369,0.35,0.4));
#31134=CARTESIAN_POINT('',(0.404145188432738,0.,0.4));
#31135=CARTESIAN_POINT('',(-0.202072594216369,0.35,0.4));
#31136=CARTESIAN_POINT('',(0.202072594216369,0.35,0.4));
#31137=CARTESIAN_POINT('',(-0.404145188432738,5.55111512312578E-17,0.4));
#31138=CARTESIAN_POINT('',(-0.202072594216369,0.35,0.4));
#31139=CARTESIAN_POINT('',(-0.202072594216369,-0.35,0.4));
#31140=CARTESIAN_POINT('',(-0.404145188432738,4.94935111404957E-17,0.4));
#31141=CARTESIAN_POINT('',(-0.202072594216369,-0.35,0.4));
#31142=CARTESIAN_POINT('Origin',(-0.202072594216369,-0.35,0.));
#31143=CARTESIAN_POINT('',(-0.202072594216369,-0.35,0.));
#31144=CARTESIAN_POINT('',(0.202072594216369,-0.35,0.));
#31145=CARTESIAN_POINT('',(-0.202072594216369,-0.35,0.));
#31146=CARTESIAN_POINT('',(0.202072594216369,-0.35,0.));
#31147=CARTESIAN_POINT('',(-0.202072594216369,-0.35,0.));
#31148=CARTESIAN_POINT('Origin',(-0.404145188432738,4.94935111404957E-17,
0.));
#31149=CARTESIAN_POINT('',(-0.404145188432738,4.94935111404957E-17,0.));
#31150=CARTESIAN_POINT('',(-0.404145188432738,4.94935111404957E-17,0.));
#31151=CARTESIAN_POINT('',(-0.404145188432738,4.94935111404957E-17,0.));
#31152=CARTESIAN_POINT('Origin',(-0.202072594216369,0.35,0.));
#31153=CARTESIAN_POINT('',(-0.202072594216369,0.35,0.));
#31154=CARTESIAN_POINT('',(-0.202072594216369,0.35,0.));
#31155=CARTESIAN_POINT('',(-0.202072594216369,0.35,0.));
#31156=CARTESIAN_POINT('Origin',(0.202072594216369,0.35,0.));
#31157=CARTESIAN_POINT('',(0.202072594216369,0.35,0.));
#31158=CARTESIAN_POINT('',(0.202072594216369,0.35,0.));
#31159=CARTESIAN_POINT('',(0.202072594216369,0.35,0.));
#31160=CARTESIAN_POINT('Origin',(0.404145188432738,0.,0.));
#31161=CARTESIAN_POINT('',(0.404145188432738,0.,0.));
#31162=CARTESIAN_POINT('',(0.404145188432738,0.,0.));
#31163=CARTESIAN_POINT('',(0.404145188432738,0.,0.));
#31164=CARTESIAN_POINT('Origin',(0.202072594216369,-0.35,0.));
#31165=CARTESIAN_POINT('',(0.202072594216369,-0.35,0.));
#31166=CARTESIAN_POINT('Origin',(0.,0.,0.));
#31544=UNCERTAINTY_MEASURE_WITH_UNIT(LENGTH_MEASURE(0.001),#31567,
'DISTANCE_ACCURACY_VALUE',
'Maximum model space distance between geometric entities at asserted c
onnectivities');
#31549=UNCERTAINTY_MEASURE_WITH_UNIT(LENGTH_MEASURE(0.001),#31567,
'DISTANCE_ACCURACY_VALUE',
'Maximum model space distance between geometric entities at asserted c
onnectivities');
#31561=(
GEOMETRIC_REPRESENTATION_CONTEXT(3)
GLOBAL_UNCERTAINTY_ASSIGNED_CONTEXT((#31544))
GLOBAL_UNIT_ASSIGNED_CONTEXT((#31567,#31569,#31570))
REPRESENTATION_CONTEXT('','3D')
);
#31566=(
GEOMETRIC_REPRESENTATION_CONTEXT(3)
GLOBAL_UNCERTAINTY_ASSIGNED_CONTEXT((#31549))
GLOBAL_UNIT_ASSIGNED_CONTEXT((#31567,#31569,#31570))
REPRESENTATION_CONTEXT('','3D')
);
#31567=(
LENGTH_UNIT()
NAMED_UNIT(*)
SI_UNIT(.CENTI.,.METRE.)
);
#31569=(
NAMED_UNIT(*)
PLANE_ANGLE_UNIT()
SI_UNIT($,.RADIAN.)
);
#31570=(
NAMED_UNIT(*)
SI_UNIT($,.STERADIAN.)
SOLID_ANGLE_UNIT()
);
#31582=SHAPE_DEFINITION_REPRESENTATION(#31598,#31646);
#31598=PRODUCT_DEFINITION_SHAPE('',$,#31663);
#31646=SHAPE_REPRESENTATION('',(#6143),#31561);
#31651=PRODUCT_DEFINITION_CONTEXT('part definition',#31701,'design');
#31663=PRODUCT_DEFINITION('Hex nut M4','Hex nut M4',#31679,#31651);
#31679=PRODUCT_DEFINITION_FORMATION('',$,#31714);
#31701=APPLICATION_CONTEXT(
'Core Data for Automotive Mechanical Design Process');
#31702=PRODUCT_CONTEXT('part definition',#31701,'mechanical');
#31714=PRODUCT('Hex nut M4','Hex nut M4',$,(#31702));
#31720=PRESENTATION_STYLE_ASSIGNMENT((#31727));
#31727=SURFACE_STYLE_USAGE(.BOTH.,#31734);
#31734=SURFACE_SIDE_STYLE('',(#31741));
#31741=SURFACE_STYLE_FILL_AREA(#31748);
#31748=FILL_AREA_STYLE('Opaque(155,165,179)',(#31755));
#31755=FILL_AREA_STYLE_COLOUR('Opaque(155,165,179)',#31762);
#31762=COLOUR_RGB('Opaque(155,165,179)',0.607843137254902,0.647058823529412,
0.701960784313725);
ENDSEC;
END-ISO-10303-21;
